ISO-10303-21;
HEADER;
/* Generated by software containing ST-Developer
 * from STEP Tools, Inc. (www.steptools.com) 
 */

FILE_DESCRIPTION(
/* description */ ('Independent eighteen-tube parallel-flow evaporator geometry. Repeated
 machined headers and gasketed service covers, eighteen copper tubes, 
twenty-nine punched fins, threaded hose connections and bolted mountin
g feet. Native editable features and instanced parts. Braze details, w
orking fluid, pressure and thermal ratings require engineering selecti
on.'),
/* implementation_level */ '2;1');

FILE_NAME(
/* name */ 'Socket head cap screw M6x12.step',
/* time_stamp */ '2026-11-08T20:53:59-08:00',
/* author */ (''),
/* organization */ (''),
/* preprocessor_version */ 'ST-DEVELOPER v20.2',
/* originating_system */ 'Autodesk Translation Framework v15.17.0.0',
/* authorisation */ '');

FILE_SCHEMA (('AUTOMOTIVE_DESIGN { 1 0 10303 214 3 1 1 }'));
ENDSEC;

DATA;
#10=MECHANICAL_DESIGN_GEOMETRIC_PRESENTATION_REPRESENTATION('',(#340),#42620);
#312=CONICAL_SURFACE('',#11140,2.5,0.785398163397449);
#320=SHAPE_REPRESENTATION_RELATIONSHIP('SRR','None',#42730,#330);
#330=ADVANCED_BREP_SHAPE_REPRESENTATION('',(#350),#42617);
#340=STYLED_ITEM('',(#42784),#350);
#350=MANIFOLD_SOLID_BREP('Body1',#10390);
#473=FACE_BOUND('',#1762,.T.);
#474=FACE_BOUND('',#1765,.T.);
#557=PLANE('',#11146);
#558=PLANE('',#11147);
#559=PLANE('',#11148);
#560=PLANE('',#11149);
#561=PLANE('',#11150);
#562=PLANE('',#11151);
#563=PLANE('',#11152);
#564=PLANE('',#11153);
#565=PLANE('',#11157);
#566=PLANE('',#11158);
#599=B_SPLINE_SURFACE_WITH_KNOTS('',3,3,((#38873,#38874,#38875,#38876,#38877,
#38878,#38879,#38880,#38881,#38882,#38883,#38884,#38885,#38886,#38887,#38888,
#38889,#38890,#38891,#38892,#38893,#38894,#38895,#38896,#38897,#38898,#38899,
#38900,#38901,#38902,#38903,#38904,#38905,#38906,#38907,#38908,#38909,#38910,
#38911,#38912,#38913,#38914,#38915,#38916,#38917,#38918,#38919,#38920,#38921,
#38922,#38923,#38924,#38925,#38926,#38927,#38928,#38929,#38930,#38931,#38932,
#38933,#38934,#38935,#38936,#38937,#38938,#38939,#38940,#38941,#38942,#38943,
#38944,#38945,#38946,#38947,#38948,#38949),(#38950,#38951,#38952,#38953,
#38954,#38955,#38956,#38957,#38958,#38959,#38960,#38961,#38962,#38963,#38964,
#38965,#38966,#38967,#38968,#38969,#38970,#38971,#38972,#38973,#38974,#38975,
#38976,#38977,#38978,#38979,#38980,#38981,#38982,#38983,#38984,#38985,#38986,
#38987,#38988,#38989,#38990,#38991,#38992,#38993,#38994,#38995,#38996,#38997,
#38998,#38999,#39000,#39001,#39002,#39003,#39004,#39005,#39006,#39007,#39008,
#39009,#39010,#39011,#39012,#39013,#39014,#39015,#39016,#39017,#39018,#39019,
#39020,#39021,#39022,#39023,#39024,#39025,#39026),(#39027,#39028,#39029,
#39030,#39031,#39032,#39033,#39034,#39035,#39036,#39037,#39038,#39039,#39040,
#39041,#39042,#39043,#39044,#39045,#39046,#39047,#39048,#39049,#39050,#39051,
#39052,#39053,#39054,#39055,#39056,#39057,#39058,#39059,#39060,#39061,#39062,
#39063,#39064,#39065,#39066,#39067,#39068,#39069,#39070,#39071,#39072,#39073,
#39074,#39075,#39076,#39077,#39078,#39079,#39080,#39081,#39082,#39083,#39084,
#39085,#39086,#39087,#39088,#39089,#39090,#39091,#39092,#39093,#39094,#39095,
#39096,#39097,#39098,#39099,#39100,#39101,#39102,#39103),(#39104,#39105,
#39106,#39107,#39108,#39109,#39110,#39111,#39112,#39113,#39114,#39115,#39116,
#39117,#39118,#39119,#39120,#39121,#39122,#39123,#39124,#39125,#39126,#39127,
#39128,#39129,#39130,#39131,#39132,#39133,#39134,#39135,#39136,#39137,#39138,
#39139,#39140,#39141,#39142,#39143,#39144,#39145,#39146,#39147,#39148,#39149,
#39150,#39151,#39152,#39153,#39154,#39155,#39156,#39157,#39158,#39159,#39160,
#39161,#39162,#39163,#39164,#39165,#39166,#39167,#39168,#39169,#39170,#39171,
#39172,#39173,#39174,#39175,#39176,#39177,#39178,#39179,#39180)),
 .UNSPECIFIED.,.F.,.F.,.F.,(4,4),(4,1,1,1,1,1,1,1,1,1,1,1,1,1,1,1,1,1,1,
1,1,1,1,1,1,1,1,1,1,1,1,1,1,1,1,1,1,1,1,1,1,1,1,1,1,1,1,1,1,1,1,1,1,1,1,
1,1,1,1,1,1,1,1,1,1,1,1,1,1,1,1,1,1,1,4),(0.,0.0658467982010768),(11.6150328478182,
12.6023632471184,13.5896936464185,14.5770240457187,15.5643544450188,16.551684844319,
17.5390152436191,18.5263456429193,19.5136760422194,20.5010064415196,21.4883368408197,
22.4756672401199,23.46299763942,24.4503280387202,25.4376584380203,26.4249888373205,
27.4123192366206,28.3996496359208,29.3869800352209,30.3743104345211,31.3616408338212,
32.3489712331214,33.3363016324215,34.3236320317217,35.3109624310218,36.298292830322,
37.2856232296221,38.2729536289223,39.2602840282224,40.2476144275226,41.2349448268227,
42.2222752261229,43.209605625423,44.1969360247232,45.1842664240233,46.1715968233235,
47.1589272226236,48.1462576219238,49.1335880212239,50.1209184205241,51.1082488198242,
52.0955792191244,53.0829096184245,54.0702400177247,55.0575704170248,56.0449008163249,
57.0322312156251,58.0195616149252,59.0068920142254,59.9942224135255,60.9815528128257,
61.9688832121258,62.956213611426,63.9435440107261,64.9308744100263,65.9182048093264,
66.9055352086266,67.8928656079267,68.8801960072269,69.867526406527,70.8548568058272,
71.8421872051273,72.8295176044275,73.8168480037276,74.8041784030278,75.7915088023279,
76.7788392016281,77.7661696009282,78.7535000002284,79.7408303995285,80.7281607988287,
81.7154911981288,82.702821597429,83.6901519967291,84.6774823960293),
 .UNSPECIFIED.);
#600=B_SPLINE_SURFACE_WITH_KNOTS('',3,3,((#39309,#39310,#39311,#39312,#39313,
#39314,#39315,#39316,#39317,#39318,#39319,#39320,#39321,#39322,#39323,#39324,
#39325,#39326,#39327,#39328,#39329,#39330,#39331,#39332,#39333,#39334,#39335,
#39336,#39337,#39338,#39339,#39340,#39341,#39342,#39343,#39344,#39345,#39346,
#39347,#39348,#39349,#39350,#39351,#39352,#39353,#39354,#39355,#39356,#39357,
#39358,#39359,#39360,#39361,#39362,#39363,#39364,#39365,#39366,#39367,#39368,
#39369,#39370,#39371,#39372,#39373,#39374,#39375,#39376,#39377,#39378,#39379,
#39380,#39381,#39382,#39383,#39384,#39385,#39386,#39387),(#39388,#39389,
#39390,#39391,#39392,#39393,#39394,#39395,#39396,#39397,#39398,#39399,#39400,
#39401,#39402,#39403,#39404,#39405,#39406,#39407,#39408,#39409,#39410,#39411,
#39412,#39413,#39414,#39415,#39416,#39417,#39418,#39419,#39420,#39421,#39422,
#39423,#39424,#39425,#39426,#39427,#39428,#39429,#39430,#39431,#39432,#39433,
#39434,#39435,#39436,#39437,#39438,#39439,#39440,#39441,#39442,#39443,#39444,
#39445,#39446,#39447,#39448,#39449,#39450,#39451,#39452,#39453,#39454,#39455,
#39456,#39457,#39458,#39459,#39460,#39461,#39462,#39463,#39464,#39465,#39466),
(#39467,#39468,#39469,#39470,#39471,#39472,#39473,#39474,#39475,#39476,
#39477,#39478,#39479,#39480,#39481,#39482,#39483,#39484,#39485,#39486,#39487,
#39488,#39489,#39490,#39491,#39492,#39493,#39494,#39495,#39496,#39497,#39498,
#39499,#39500,#39501,#39502,#39503,#39504,#39505,#39506,#39507,#39508,#39509,
#39510,#39511,#39512,#39513,#39514,#39515,#39516,#39517,#39518,#39519,#39520,
#39521,#39522,#39523,#39524,#39525,#39526,#39527,#39528,#39529,#39530,#39531,
#39532,#39533,#39534,#39535,#39536,#39537,#39538,#39539,#39540,#39541,#39542,
#39543,#39544,#39545),(#39546,#39547,#39548,#39549,#39550,#39551,#39552,
#39553,#39554,#39555,#39556,#39557,#39558,#39559,#39560,#39561,#39562,#39563,
#39564,#39565,#39566,#39567,#39568,#39569,#39570,#39571,#39572,#39573,#39574,
#39575,#39576,#39577,#39578,#39579,#39580,#39581,#39582,#39583,#39584,#39585,
#39586,#39587,#39588,#39589,#39590,#39591,#39592,#39593,#39594,#39595,#39596,
#39597,#39598,#39599,#39600,#39601,#39602,#39603,#39604,#39605,#39606,#39607,
#39608,#39609,#39610,#39611,#39612,#39613,#39614,#39615,#39616,#39617,#39618,
#39619,#39620,#39621,#39622,#39623,#39624)),.UNSPECIFIED.,.F.,.F.,.F.,(4,
4),(4,1,1,1,1,1,1,1,1,1,1,1,1,1,1,1,1,1,1,1,1,1,1,1,1,1,1,1,1,1,1,1,1,1,
1,1,1,1,1,1,1,1,1,1,1,1,1,1,1,1,1,1,1,1,1,1,1,1,1,1,1,1,1,1,1,1,1,1,1,1,
1,1,1,1,1,1,4),(0.,0.0658467982010768),(8.30747755240104,9.2960444961263,
10.2846114398516,11.2731783835768,12.2617453273021,13.2503122710274,14.2388792147526,
15.2274461584779,16.2160131022032,17.2045800459284,18.1931469896537,19.181713933379,
20.1702808771042,21.1588478208295,22.1474147645547,23.13598170828,24.1245486520053,
25.1131155957305,26.1016825394558,27.0902494831811,28.0788164269063,29.0673833706316,
30.0559503143569,31.0445172580821,32.0330842018074,33.0216511455327,34.0102180892579,
34.9987850329832,35.9873519767085,36.9759189204337,37.964485864159,38.9530528078842,
39.9416197516095,40.9301866953348,41.91875363906,42.9073205827853,43.8958875265106,
44.8844544702358,45.8730214139611,46.8615883576864,47.8501553014116,48.8387222451369,
49.8272891888622,50.8158561325874,51.8044230763127,52.792990020038,53.7815569637632,
54.7701239074885,55.7586908512138,56.747257794939,57.7358247386643,58.7243916823895,
59.7129586261148,60.7015255698401,61.6900925135653,62.6786594572906,63.6672264010159,
64.6557933447411,65.6443602884664,66.6329272321917,67.6214941759169,68.6100611196422,
69.5986280633675,70.5871950070927,71.575761950818,72.5643288945433,73.5528958382685,
74.5414627819938,75.530029725719,76.5185966694443,77.5071636131696,78.4957305568948,
79.4842975006201,80.4728644443454,81.4614313880706,82.4499983317959,83.4385652755212),
 .UNSPECIFIED.);
#1063=FACE_OUTER_BOUND('',#1727,.T.);
#1064=FACE_OUTER_BOUND('',#1728,.T.);
#1065=FACE_OUTER_BOUND('',#1729,.T.);
#1066=FACE_OUTER_BOUND('',#1730,.T.);
#1067=FACE_OUTER_BOUND('',#1731,.T.);
#1068=FACE_OUTER_BOUND('',#1732,.T.);
#1069=FACE_OUTER_BOUND('',#1733,.T.);
#1070=FACE_OUTER_BOUND('',#1734,.T.);
#1071=FACE_OUTER_BOUND('',#1735,.T.);
#1072=FACE_OUTER_BOUND('',#1736,.T.);
#1073=FACE_OUTER_BOUND('',#1737,.T.);
#1074=FACE_OUTER_BOUND('',#1738,.T.);
#1075=FACE_OUTER_BOUND('',#1739,.T.);
#1076=FACE_OUTER_BOUND('',#1740,.T.);
#1077=FACE_OUTER_BOUND('',#1741,.T.);
#1078=FACE_OUTER_BOUND('',#1742,.T.);
#1079=FACE_OUTER_BOUND('',#1743,.T.);
#1080=FACE_OUTER_BOUND('',#1744,.T.);
#1081=FACE_OUTER_BOUND('',#1745,.T.);
#1082=FACE_OUTER_BOUND('',#1746,.T.);
#1083=FACE_OUTER_BOUND('',#1747,.T.);
#1084=FACE_OUTER_BOUND('',#1748,.T.);
#1085=FACE_OUTER_BOUND('',#1749,.T.);
#1086=FACE_OUTER_BOUND('',#1750,.T.);
#1087=FACE_OUTER_BOUND('',#1751,.T.);
#1088=FACE_OUTER_BOUND('',#1752,.T.);
#1089=FACE_OUTER_BOUND('',#1753,.T.);
#1090=FACE_OUTER_BOUND('',#1754,.T.);
#1091=FACE_OUTER_BOUND('',#1755,.T.);
#1092=FACE_OUTER_BOUND('',#1756,.T.);
#1093=FACE_OUTER_BOUND('',#1757,.T.);
#1094=FACE_OUTER_BOUND('',#1758,.T.);
#1095=FACE_OUTER_BOUND('',#1759,.T.);
#1096=FACE_OUTER_BOUND('',#1760,.T.);
#1097=FACE_OUTER_BOUND('',#1761,.T.);
#1098=FACE_OUTER_BOUND('',#1763,.T.);
#1099=FACE_OUTER_BOUND('',#1764,.T.);
#1100=FACE_OUTER_BOUND('',#1766,.T.);
#1727=EDGE_LOOP('',(#9005,#9006,#9007,#9008));
#1728=EDGE_LOOP('',(#9009,#9010,#9011,#9012));
#1729=EDGE_LOOP('',(#9013,#9014,#9015,#9016));
#1730=EDGE_LOOP('',(#9017,#9018,#9019,#9020));
#1731=EDGE_LOOP('',(#9021,#9022,#9023,#9024));
#1732=EDGE_LOOP('',(#9025,#9026,#9027,#9028));
#1733=EDGE_LOOP('',(#9029,#9030,#9031,#9032));
#1734=EDGE_LOOP('',(#9033,#9034,#9035,#9036));
#1735=EDGE_LOOP('',(#9037,#9038,#9039,#9040));
#1736=EDGE_LOOP('',(#9041,#9042,#9043,#9044));
#1737=EDGE_LOOP('',(#9045,#9046,#9047,#9048));
#1738=EDGE_LOOP('',(#9049,#9050,#9051,#9052));
#1739=EDGE_LOOP('',(#9053,#9054,#9055,#9056));
#1740=EDGE_LOOP('',(#9057,#9058,#9059,#9060));
#1741=EDGE_LOOP('',(#9061,#9062,#9063,#9064));
#1742=EDGE_LOOP('',(#9065,#9066,#9067,#9068));
#1743=EDGE_LOOP('',(#9069,#9070,#9071,#9072));
#1744=EDGE_LOOP('',(#9073,#9074,#9075,#9076));
#1745=EDGE_LOOP('',(#9077,#9078,#9079,#9080));
#1746=EDGE_LOOP('',(#9081,#9082,#9083,#9084));
#1747=EDGE_LOOP('',(#9085,#9086,#9087,#9088));
#1748=EDGE_LOOP('',(#9089,#9090,#9091,#9092));
#1749=EDGE_LOOP('',(#9093,#9094,#9095,#9096,#9097,#9098,#9099,#9100));
#1750=EDGE_LOOP('',(#9101,#9102,#9103,#9104,#9105,#9106,#9107,#9108,#9109,
#9110,#9111,#9112,#9113,#9114,#9115,#9116,#9117,#9118,#9119,#9120,#9121,
#9122,#9123,#9124,#9125,#9126));
#1751=EDGE_LOOP('',(#9127,#9128,#9129,#9130));
#1752=EDGE_LOOP('',(#9131,#9132,#9133,#9134,#9135,#9136,#9137,#9138,#9139,
#9140,#9141,#9142,#9143,#9144,#9145,#9146,#9147,#9148,#9149,#9150,#9151,
#9152,#9153,#9154,#9155,#9156,#9157));
#1753=EDGE_LOOP('',(#9158,#9159,#9160,#9161));
#1754=EDGE_LOOP('',(#9162,#9163,#9164,#9165));
#1755=EDGE_LOOP('',(#9166,#9167,#9168,#9169));
#1756=EDGE_LOOP('',(#9170,#9171,#9172,#9173));
#1757=EDGE_LOOP('',(#9174,#9175,#9176,#9177));
#1758=EDGE_LOOP('',(#9178,#9179,#9180,#9181));
#1759=EDGE_LOOP('',(#9182,#9183,#9184,#9185));
#1760=EDGE_LOOP('',(#9186,#9187,#9188,#9189,#9190,#9191));
#1761=EDGE_LOOP('',(#9192));
#1762=EDGE_LOOP('',(#9193,#9194,#9195,#9196));
#1763=EDGE_LOOP('',(#9197,#9198,#9199,#9200));
#1764=EDGE_LOOP('',(#9201));
#1765=EDGE_LOOP('',(#9202,#9203,#9204,#9205,#9206,#9207));
#1766=EDGE_LOOP('',(#9208));
#1988=CIRCLE('',#11117,2.942);
#1989=CIRCLE('',#11129,2.37175);
#1990=CIRCLE('',#11141,2.942);
#1991=CIRCLE('',#11142,2.);
#1992=CIRCLE('',#11144,2.37175);
#1993=CIRCLE('',#11154,5.);
#1994=CIRCLE('',#11156,5.);
#2700=B_SPLINE_CURVE_WITH_KNOTS('',3,(#37767,#37768,#37769,#37770,#37771,
#37772,#37773,#37774,#37775,#37776),.UNSPECIFIED.,.F.,.F.,(4,3,3,4),(-4.09293042013066,
-3.9493215972006,-2.96199119790045,-2.06863817490914),.UNSPECIFIED.);
#2701=B_SPLINE_CURVE_WITH_KNOTS('',3,(#37779,#37780,#37781,#37782,#37783,
#37784,#37785),.UNSPECIFIED.,.F.,.F.,(4,3,4),(0.,0.988566943725272,1.11730040836823),
 .UNSPECIFIED.);
#2702=B_SPLINE_CURVE_WITH_KNOTS('',3,(#37790,#37791,#37792,#37793,#37794,
#37795,#37796,#37797,#37798,#37799,#37800,#37801,#37802,#37803,#37804,#37805,
#37806,#37807,#37808,#37809,#37810,#37811),.UNSPECIFIED.,.F.,.F.,(4,3,3,
3,3,3,3,4),(-10.3761157273102,-9.87330399300149,-8.88597359370134,-7.89864319440119,
-6.91131279510104,-5.92398239580089,-4.93665199650074,-4.09293042013066),
 .UNSPECIFIED.);
#2703=B_SPLINE_CURVE_WITH_KNOTS('',3,(#37812,#37813,#37814,#37815,#37816,
#37817,#37818,#37819,#37820,#37821,#37822,#37823,#37824,#37825,#37826,#37827,
#37828,#37829,#37830,#37831,#37832,#37833),.UNSPECIFIED.,.F.,.F.,(4,3,3,
3,3,3,3,4),(1.11730040836823,1.97713388745054,2.9657008311758,3.95426777490106,
4.94283471862632,5.93140166235159,6.91996860607685,7.40048571554782),
 .UNSPECIFIED.);
#2704=B_SPLINE_CURVE_WITH_KNOTS('',3,(#37838,#37839,#37840,#37841,#37842,
#37843,#37844,#37845,#37846,#37847,#37848,#37849,#37850,#37851,#37852,#37853,
#37854,#37855,#37856,#37857,#37858,#37859),.UNSPECIFIED.,.F.,.F.,(4,3,3,
3,3,3,3,4),(-16.6593010344898,-15.7972863888024,-14.8099559895022,-13.8226255902021,
-12.8352951909019,-11.8479647916018,-10.8606343923016,-10.3761157273102),
 .UNSPECIFIED.);
#2705=B_SPLINE_CURVE_WITH_KNOTS('',3,(#37860,#37861,#37862,#37863,#37864,
#37865,#37866,#37867,#37868,#37869,#37870,#37871,#37872,#37873,#37874,#37875,
#37876,#37877,#37878,#37879,#37880,#37881),.UNSPECIFIED.,.F.,.F.,(4,3,3,
3,3,3,3,4),(7.40048571554782,7.90853554980211,8.89710249352738,9.88566943725264,
10.8742363809779,11.8628033247032,12.8513702684284,13.6836710227274),
 .UNSPECIFIED.);
#2706=B_SPLINE_CURVE_WITH_KNOTS('',3,(#37886,#37887,#37888,#37889,#37890,
#37891,#37892,#37893,#37894,#37895,#37896,#37897,#37898,#37899,#37900,#37901,
#37902,#37903,#37904,#37905,#37906,#37907,#37908,#37909,#37910),
 .UNSPECIFIED.,.F.,.F.,(4,3,3,3,3,3,3,3,4),(-22.9424863416694,-22.7085991839034,
-21.7212687846033,-20.7339383853031,-19.746607986003,-18.7592775867028,
-17.7719471874027,-16.7846167881025,-16.6593010344898),.UNSPECIFIED.);
#2707=B_SPLINE_CURVE_WITH_KNOTS('',3,(#37911,#37912,#37913,#37914,#37915,
#37916,#37917,#37918,#37919,#37920,#37921,#37922,#37923,#37924,#37925,#37926,
#37927,#37928,#37929,#37930,#37931,#37932,#37933,#37934,#37935),
 .UNSPECIFIED.,.F.,.F.,(4,3,3,3,3,3,3,3,4),(13.6836710227274,13.8399372121537,
14.828504155879,15.8170710996042,16.8056380433295,17.7942049870548,18.78277193078,
19.7713388745053,19.966856329907),.UNSPECIFIED.);
#2708=B_SPLINE_CURVE_WITH_KNOTS('',3,(#37940,#37941,#37942,#37943,#37944,
#37945,#37946,#37947,#37948,#37949,#37950,#37951,#37952,#37953,#37954,#37955,
#37956,#37957,#37958,#37959,#37960,#37961),.UNSPECIFIED.,.F.,.F.,(4,3,3,
3,3,3,3,4),(-29.225671648849,-28.6325815797043,-27.6452511804042,-26.657920781104,
-25.6705903818039,-24.6832599825037,-23.6959295832036,-22.9424863416694),
 .UNSPECIFIED.);
#2709=B_SPLINE_CURVE_WITH_KNOTS('',3,(#37962,#37963,#37964,#37965,#37966,
#37967,#37968,#37969,#37970,#37971,#37972,#37973,#37974,#37975,#37976,#37977,
#37978,#37979,#37980,#37981,#37982,#37983),.UNSPECIFIED.,.F.,.F.,(4,3,3,
3,3,3,3,4),(19.966856329907,20.7599058182306,21.7484727619558,22.7370397056811,
23.7256066494064,24.7141735931316,25.7027405368569,26.2500416370866),
 .UNSPECIFIED.);
#2710=B_SPLINE_CURVE_WITH_KNOTS('',3,(#37988,#37989,#37990,#37991,#37992,
#37993,#37994,#37995,#37996,#37997,#37998,#37999,#38000,#38001,#38002,#38003,
#38004,#38005,#38006,#38007,#38008,#38009),.UNSPECIFIED.,.F.,.F.,(4,3,3,
3,3,3,3,4),(-35.5088569560286,-34.5565639755052,-33.5692335762051,-32.5819031769049,
-31.5945727776048,-30.6072423783046,-29.6199119790045,-29.225671648849),
 .UNSPECIFIED.);
#2711=B_SPLINE_CURVE_WITH_KNOTS('',3,(#38010,#38011,#38012,#38013,#38014,
#38015,#38016,#38017,#38018,#38019,#38020,#38021,#38022,#38023,#38024,#38025,
#38026,#38027,#38028,#38029,#38030,#38031),.UNSPECIFIED.,.F.,.F.,(4,3,3,
3,3,3,3,4),(26.2500416370866,26.6913074805822,27.6798744243074,28.6684413680327,
29.6570083117579,30.6455752554832,31.6341421992085,32.5332269442662),
 .UNSPECIFIED.);
#2712=B_SPLINE_CURVE_WITH_KNOTS('',3,(#38036,#38037,#38038,#38039,#38040,
#38041,#38042,#38043,#38044,#38045,#38046,#38047,#38048,#38049,#38050,#38051,
#38052,#38053,#38054,#38055,#38056,#38057,#38058,#38059,#38060),
 .UNSPECIFIED.,.F.,.F.,(4,3,3,3,3,3,3,3,4),(-41.7920422632082,-41.4678767706063,
-40.4805463713061,-39.4932159720059,-38.5058855727058,-37.5185551734057,
-36.5312247741055,-35.5438943748054,-35.5088569560286),.UNSPECIFIED.);
#2713=B_SPLINE_CURVE_WITH_KNOTS('',3,(#38061,#38062,#38063,#38064,#38065,
#38066,#38067,#38068,#38069,#38070,#38071,#38072,#38073,#38074,#38075,#38076,
#38077,#38078,#38079,#38080,#38081,#38082,#38083,#38084,#38085),
 .UNSPECIFIED.,.F.,.F.,(4,3,3,3,3,3,3,3,4),(32.5332269442662,32.6227091429337,
33.611276086659,34.5998430303843,35.5884099741095,36.5769769178348,37.5655438615601,
38.5541108052853,38.8164122514458),.UNSPECIFIED.);
#2714=B_SPLINE_CURVE_WITH_KNOTS('',3,(#38090,#38091,#38092,#38093,#38094,
#38095,#38096,#38097,#38098,#38099,#38100,#38101,#38102,#38103,#38104,#38105,
#38106,#38107,#38108,#38109,#38110,#38111),.UNSPECIFIED.,.F.,.F.,(4,3,3,
3,3,3,3,4),(-48.0752275703878,-47.3918591664071,-46.404528767107,-45.4171983678069,
-44.4298679685067,-43.4425375692066,-42.4552071699064,-41.7920422632082),
 .UNSPECIFIED.);
#2715=B_SPLINE_CURVE_WITH_KNOTS('',3,(#38112,#38113,#38114,#38115,#38116,
#38117,#38118,#38119,#38120,#38121,#38122,#38123,#38124,#38125,#38126,#38127,
#38128,#38129,#38130,#38131,#38132,#38133),.UNSPECIFIED.,.F.,.F.,(4,3,3,
3,3,3,3,4),(38.8164122514458,39.5426777490106,40.5312446927359,41.5198116364611,
42.5083785801864,43.4969455239117,44.4855124676369,45.0995975586253),
 .UNSPECIFIED.);
#2716=B_SPLINE_CURVE_WITH_KNOTS('',3,(#38138,#38139,#38140,#38141,#38142,
#38143,#38144,#38145,#38146,#38147,#38148,#38149,#38150,#38151,#38152,#38153,
#38154,#38155,#38156,#38157,#38158,#38159,#38160,#38161,#38162),
 .UNSPECIFIED.,.F.,.F.,(4,3,3,3,3,3,3,3,4),(-54.3584128775674,-54.3031719615082,
-53.315841562208,-52.3285111629079,-51.3411807636077,-50.3538503643076,
-49.3665199650074,-48.3791895657073,-48.0752275703878),.UNSPECIFIED.);
#2717=B_SPLINE_CURVE_WITH_KNOTS('',3,(#38163,#38164,#38165,#38166,#38167,
#38168,#38169,#38170,#38171,#38172,#38173,#38174,#38175,#38176,#38177,#38178,
#38179,#38180,#38181,#38182,#38183,#38184),.UNSPECIFIED.,.F.,.F.,(4,3,3,
3,3,3,3,4),(45.0995975586253,45.4740794113622,46.4626463550875,47.4512132988127,
48.439780242538,49.4283471862633,50.4169141299885,51.3827828658049),
 .UNSPECIFIED.);
#2718=B_SPLINE_CURVE_WITH_KNOTS('',3,(#38189,#38190,#38191,#38192,#38193,
#38194,#38195,#38196,#38197,#38198,#38199,#38200,#38201,#38202,#38203,#38204,
#38205,#38206,#38207,#38208,#38209,#38210),.UNSPECIFIED.,.F.,.F.,(4,3,3,
3,3,3,3,4),(-60.641598184747,-60.2271543573091,-59.2398239580089,-58.2524935587088,
-57.2651631594086,-56.2778327601085,-55.2905023608083,-54.3584128775674),
 .UNSPECIFIED.);
#2719=B_SPLINE_CURVE_WITH_KNOTS('',3,(#38211,#38212,#38213,#38214,#38215,
#38216,#38217,#38218,#38219,#38220,#38221,#38222,#38223,#38224,#38225,#38226,
#38227,#38228,#38229,#38230,#38231,#38232,#38233,#38234,#38235),
 .UNSPECIFIED.,.F.,.F.,(4,3,3,3,3,3,3,3,4),(51.3827828658049,51.4054810737138,
52.394048017439,53.3826149611643,54.3711819048896,55.3597488486148,56.3483157923401,
57.3368827360654,57.6659681729845),.UNSPECIFIED.);
#2720=B_SPLINE_CURVE_WITH_KNOTS('',3,(#38240,#38241,#38242,#38243,#38244,
#38245,#38246,#38247,#38248,#38249,#38250,#38251,#38252,#38253,#38254,#38255,
#38256,#38257,#38258,#38259,#38260,#38261),.UNSPECIFIED.,.F.,.F.,(4,3,3,
3,3,3,3,4),(-66.9247834919266,-66.15113675311,-65.1638063538098,-64.1764759545097,
-63.1891455552095,-62.2018151559094,-61.2144847566092,-60.641598184747),
 .UNSPECIFIED.);
#2721=B_SPLINE_CURVE_WITH_KNOTS('',3,(#38262,#38263,#38264,#38265,#38266,
#38267,#38268,#38269,#38270,#38271,#38272,#38273,#38274,#38275,#38276,#38277,
#38278,#38279,#38280,#38281,#38282,#38283),.UNSPECIFIED.,.F.,.F.,(4,3,3,
3,3,3,3,4),(57.6659681729845,58.3254496797906,59.3140166235159,60.3025835672412,
61.2911505109664,62.2797174546917,63.268284398417,63.9491534801641),
 .UNSPECIFIED.);
#2722=B_SPLINE_CURVE_WITH_KNOTS('',3,(#38289,#38290,#38291,#38292,#38293,
#38294,#38295,#38296,#38297,#38298),.UNSPECIFIED.,.F.,.F.,(4,1,1,1,1,1,
1,4),(78.5398163397448,78.7535000002284,79.7408303995285,80.7281607988287,
81.7154911981288,82.702821597429,83.6901519967291,84.6774823960293),
 .UNSPECIFIED.);
#2723=B_SPLINE_CURVE_WITH_KNOTS('',3,(#38301,#38302,#38303,#38304,#38305,
#38306,#38307,#38308),.UNSPECIFIED.,.F.,.F.,(4,1,1,1,1,4),(78.5398163397448,
79.4842975006201,80.4728644443454,81.4614313880706,82.4499983317959,83.4385652755212),
 .UNSPECIFIED.);
#2724=B_SPLINE_CURVE_WITH_KNOTS('',3,(#38313,#38314,#38315,#38316,#38317,
#38318,#38319,#38320,#38321,#38322),.UNSPECIFIED.,.F.,.F.,(4,1,1,1,1,1,
1,4),(72.2566310325653,72.8295176044275,73.8168480037276,74.8041784030278,
75.7915088023279,76.7788392016281,77.7661696009282,78.5398163397448),
 .UNSPECIFIED.);
#2725=B_SPLINE_CURVE_WITH_KNOTS('',3,(#38323,#38324,#38325,#38326,#38327,
#38328,#38329,#38330,#38331,#38332,#38333),.UNSPECIFIED.,.F.,.F.,(4,1,1,
1,1,1,1,1,4),(72.2566310325652,72.5643288945433,73.5528958382685,74.5414627819938,
75.530029725719,76.5185966694443,77.5071636131696,78.4957305568948,78.5398163397448),
 .UNSPECIFIED.);
#2726=B_SPLINE_CURVE_WITH_KNOTS('',3,(#38338,#38339,#38340,#38341,#38342,
#38343,#38344,#38345,#38346,#38347),.UNSPECIFIED.,.F.,.F.,(4,1,1,1,1,1,
1,4),(65.9734457253856,66.9055352086266,67.8928656079267,68.8801960072269,
69.867526406527,70.8548568058272,71.8421872051273,72.2566310325653),
 .UNSPECIFIED.);
#2727=B_SPLINE_CURVE_WITH_KNOTS('',3,(#38348,#38349,#38350,#38351,#38352,
#38353,#38354,#38355,#38356,#38357),.UNSPECIFIED.,.F.,.F.,(4,1,1,1,1,1,
1,4),(65.9734457253856,66.6329272321917,67.6214941759169,68.6100611196422,
69.5986280633675,70.5871950070927,71.575761950818,72.2566310325652),
 .UNSPECIFIED.);
#2728=B_SPLINE_CURVE_WITH_KNOTS('',3,(#38362,#38363,#38364,#38365,#38366,
#38367,#38368,#38369,#38370,#38371,#38372),.UNSPECIFIED.,.F.,.F.,(4,1,1,
1,1,1,1,1,4),(59.6902604182061,59.9942224135255,60.9815528128257,61.9688832121258,
62.956213611426,63.9435440107261,64.9308744100263,65.9182048093264,65.9734457253856),
 .UNSPECIFIED.);
#2729=B_SPLINE_CURVE_WITH_KNOTS('',3,(#38373,#38374,#38375,#38376,#38377,
#38378,#38379,#38380,#38381,#38382,#38383),.UNSPECIFIED.,.F.,.F.,(4,1,1,
1,1,1,1,1,4),(59.6902604182061,59.7129586261148,60.7015255698401,61.6900925135653,
62.6786594572906,63.6672264010159,64.6557933447411,65.6443602884664,65.9734457253856),
 .UNSPECIFIED.);
#2730=B_SPLINE_CURVE_WITH_KNOTS('',3,(#38388,#38389,#38390,#38391,#38392,
#38393,#38394,#38395,#38396,#38397),.UNSPECIFIED.,.F.,.F.,(4,1,1,1,1,1,
1,4),(53.4070751110265,54.0702400177247,55.0575704170248,56.0449008163249,
57.0322312156251,58.0195616149252,59.0068920142254,59.6902604182061),
 .UNSPECIFIED.);
#2731=B_SPLINE_CURVE_WITH_KNOTS('',3,(#38398,#38399,#38400,#38401,#38402,
#38403,#38404,#38405,#38406,#38407),.UNSPECIFIED.,.F.,.F.,(4,1,1,1,1,1,
1,4),(53.4070751110265,53.7815569637632,54.7701239074885,55.7586908512138,
56.747257794939,57.7358247386643,58.7243916823895,59.6902604182061),
 .UNSPECIFIED.);
#2732=B_SPLINE_CURVE_WITH_KNOTS('',3,(#38412,#38413,#38414,#38415,#38416,
#38417,#38418,#38419,#38420,#38421,#38422),.UNSPECIFIED.,.F.,.F.,(4,1,1,
1,1,1,1,1,4),(47.1238898038469,47.1589272226236,48.1462576219238,49.1335880212239,
50.1209184205241,51.1082488198242,52.0955792191244,53.0829096184245,53.4070751110265),
 .UNSPECIFIED.);
#2733=B_SPLINE_CURVE_WITH_KNOTS('',3,(#38423,#38424,#38425,#38426,#38427,
#38428,#38429,#38430,#38431,#38432),.UNSPECIFIED.,.F.,.F.,(4,1,1,1,1,1,
1,4),(47.1238898038469,47.8501553014116,48.8387222451369,49.8272891888622,
50.8158561325874,51.8044230763127,52.792990020038,53.4070751110265),
 .UNSPECIFIED.);
#2734=B_SPLINE_CURVE_WITH_KNOTS('',3,(#38437,#38438,#38439,#38440,#38441,
#38442,#38443,#38444,#38445,#38446),.UNSPECIFIED.,.F.,.F.,(4,1,1,1,1,1,
1,4),(40.8407044966673,41.2349448268227,42.2222752261229,43.209605625423,
44.1969360247232,45.1842664240233,46.1715968233235,47.1238898038469),
 .UNSPECIFIED.);
#2735=B_SPLINE_CURVE_WITH_KNOTS('',3,(#38447,#38448,#38449,#38450,#38451,
#38452,#38453,#38454,#38455,#38456,#38457),.UNSPECIFIED.,.F.,.F.,(4,1,1,
1,1,1,1,1,4),(40.8407044966673,40.9301866953348,41.91875363906,42.9073205827853,
43.8958875265106,44.8844544702358,45.8730214139611,46.8615883576864,47.1238898038469),
 .UNSPECIFIED.);
#2736=B_SPLINE_CURVE_WITH_KNOTS('',3,(#38462,#38463,#38464,#38465,#38466,
#38467,#38468,#38469,#38470,#38471),.UNSPECIFIED.,.F.,.F.,(4,1,1,1,1,1,
1,4),(34.5575191894877,35.3109624310218,36.298292830322,37.2856232296221,
38.2729536289223,39.2602840282224,40.2476144275226,40.8407044966673),
 .UNSPECIFIED.);
#2737=B_SPLINE_CURVE_WITH_KNOTS('',3,(#38472,#38473,#38474,#38475,#38476,
#38477,#38478,#38479,#38480,#38481),.UNSPECIFIED.,.F.,.F.,(4,1,1,1,1,1,
1,4),(34.5575191894877,34.9987850329832,35.9873519767085,36.9759189204337,
37.964485864159,38.9530528078842,39.9416197516095,40.8407044966673),
 .UNSPECIFIED.);
#2738=B_SPLINE_CURVE_WITH_KNOTS('',3,(#38486,#38487,#38488,#38489,#38490,
#38491,#38492,#38493,#38494,#38495,#38496),.UNSPECIFIED.,.F.,.F.,(4,1,1,
1,1,1,1,1,4),(28.2743338823081,28.3996496359208,29.3869800352209,30.3743104345211,
31.3616408338212,32.3489712331214,33.3363016324215,34.3236320317217,34.5575191894877),
 .UNSPECIFIED.);
#2739=B_SPLINE_CURVE_WITH_KNOTS('',3,(#38497,#38498,#38499,#38500,#38501,
#38502,#38503,#38504,#38505,#38506),.UNSPECIFIED.,.F.,.F.,(4,1,1,1,1,1,
1,4),(28.2743338823081,29.0673833706316,30.0559503143569,31.0445172580821,
32.0330842018074,33.0216511455327,34.0102180892579,34.5575191894877),
 .UNSPECIFIED.);
#2740=B_SPLINE_CURVE_WITH_KNOTS('',3,(#38511,#38512,#38513,#38514,#38515,
#38516,#38517,#38518,#38519,#38520),.UNSPECIFIED.,.F.,.F.,(4,1,1,1,1,1,
1,4),(21.9911485751285,22.4756672401199,23.46299763942,24.4503280387202,
25.4376584380203,26.4249888373205,27.4123192366206,28.2743338823081),
 .UNSPECIFIED.);
#2741=B_SPLINE_CURVE_WITH_KNOTS('',3,(#38521,#38522,#38523,#38524,#38525,
#38526,#38527,#38528,#38529,#38530,#38531),.UNSPECIFIED.,.F.,.F.,(4,1,1,
1,1,1,1,1,4),(21.9911485751285,22.1474147645547,23.13598170828,24.1245486520053,
25.1131155957305,26.1016825394558,27.0902494831811,28.0788164269063,28.2743338823081),
 .UNSPECIFIED.);
#2742=B_SPLINE_CURVE_WITH_KNOTS('',3,(#38536,#38537,#38538,#38539,#38540,
#38541,#38542,#38543,#38544,#38545),.UNSPECIFIED.,.F.,.F.,(4,1,1,1,1,1,
1,4),(15.7079632679489,16.551684844319,17.5390152436191,18.5263456429193,
19.5136760422194,20.5010064415196,21.4883368408197,21.9911485751285),
 .UNSPECIFIED.);
#2743=B_SPLINE_CURVE_WITH_KNOTS('',3,(#38546,#38547,#38548,#38549,#38550,
#38551,#38552,#38553,#38554,#38555),.UNSPECIFIED.,.F.,.F.,(4,1,1,1,1,1,
1,4),(15.7079632679489,16.2160131022032,17.2045800459284,18.1931469896537,
19.181713933379,20.1702808771042,21.1588478208295,21.9911485751285),
 .UNSPECIFIED.);
#2744=B_SPLINE_CURVE_WITH_KNOTS('',3,(#38558,#38559,#38560,#38561,#38562,
#38563,#38564,#38565,#38566,#38567,#38568,#38569,#38570,#38571,#38572,#38573,
#38574,#38575,#38576,#38577,#38578,#38579,#38580,#38581,#38582,#38583,#38584,
#38585,#38586,#38587,#38588,#38589,#38590,#38591,#38592,#38593,#38594,#38595,
#38596,#38597,#38598,#38599,#38600,#38601,#38602,#38603,#38604,#38605,#38606,
#38607,#38608,#38609,#38610,#38611,#38612,#38613,#38614,#38615,#38616,#38617,
#38618,#38619,#38620,#38621,#38622,#38623,#38624,#38625,#38626,#38627,#38628,
#38629,#38630,#38631,#38632,#38633,#38634,#38635,#38636,#38637,#38638,#38639,
#38640,#38641,#38642,#38643,#38644,#38645,#38646,#38647,#38648,#38649,#38650,
#38651,#38652,#38653,#38654,#38655,#38656,#38657,#38658,#38659,#38660,#38661,
#38662,#38663,#38664,#38665,#38666,#38667,#38668,#38669,#38670,#38671,#38672,
#38673,#38674,#38675,#38676,#38677,#38678,#38679,#38680,#38681,#38682,#38683,
#38684,#38685,#38686,#38687,#38688,#38689,#38690,#38691,#38692,#38693,#38694,
#38695,#38696,#38697,#38698,#38699,#38700,#38701,#38702,#38703,#38704,#38705,
#38706,#38707,#38708,#38709,#38710,#38711,#38712,#38713,#38714,#38715,#38716,
#38717,#38718,#38719,#38720,#38721,#38722,#38723,#38724,#38725,#38726,#38727,
#38728,#38729,#38730,#38731,#38732,#38733,#38734,#38735,#38736,#38737,#38738,
#38739,#38740,#38741,#38742,#38743,#38744,#38745,#38746,#38747,#38748,#38749,
#38750,#38751,#38752,#38753,#38754,#38755,#38756,#38757,#38758,#38759,#38760,
#38761,#38762,#38763,#38764,#38765,#38766,#38767,#38768,#38769,#38770,#38771,
#38772,#38773,#38774),.UNSPECIFIED.,.F.,.F.,(4,3,3,3,3,3,3,3,3,3,3,3,3,
3,3,3,3,3,3,3,3,3,3,3,3,3,3,3,3,3,3,3,3,3,3,3,3,3,3,3,3,3,3,3,3,3,3,3,3,
3,3,3,3,3,3,3,3,3,3,3,3,3,3,3,3,3,3,3,3,3,3,3,4),(-1.51155304937228,-1.48679174718013,
-1.46137597198077,-1.44942691521821,-1.44205848651244,-1.43724119559823,
-1.41130764113729,-1.38514768961224,-1.36936593028954,-1.36512230166791,
-1.33867581137855,-1.31235917608035,-1.29127511993008,-1.28073309185494,
-1.2739086628828,-1.27019106377981,-1.24488979836553,-1.21884130205047,
-1.19384888620637,-1.18291470427457,-1.17641188206357,-1.17130697868968,
-1.14451640582175,-1.11742561305122,-1.09279470361283,-1.08177565945417,
-1.07670730294613,-1.07245364414871,-1.0452101587782,-1.01890197529764,
-0.992076665792053,-0.977095538498891,-0.971310437727824,-0.944262984582137,
-0.91671696123902,-0.889051349044572,-0.8786107219546,-0.873404326505122,
-0.869185758667877,-0.841205731090746,-0.813331817877821,-0.785648584359967,
-0.771436006282574,-0.765308450445371,-0.757965350842113,-0.731019445974318,
-0.703340715547858,-0.676331238706378,-0.668063308133434,-0.663247880961674,
-0.658967945513649,-0.630690110839631,-0.602089962339152,-0.573383696958367,
-0.562618847440572,-0.556352694911719,-0.55203012393032,-0.523164492059728,
-0.494713544949419,-0.487264900816012,-0.45884309987075,-0.449622389577847,
-0.445165938771905,-0.416742684601646,-0.387755299334011,-0.358563756837841,
-0.34211828207705,-0.337697582134308,-0.308241853281341,-0.278784672736061,
-0.25000255453776,-0.226999958751515,-0.219677966288006),.UNSPECIFIED.);
#2745=B_SPLINE_CURVE_WITH_KNOTS('',3,(#38776,#38777,#38778,#38779,#38780,
#38781,#38782,#38783,#38784,#38785,#38786,#38787,#38788,#38789,#38790,#38791,
#38792,#38793,#38794,#38795,#38796,#38797,#38798,#38799,#38800,#38801,#38802,
#38803,#38804,#38805,#38806,#38807,#38808,#38809,#38810,#38811,#38812,#38813,
#38814,#38815,#38816,#38817,#38818,#38819,#38820,#38821,#38822,#38823,#38824,
#38825,#38826,#38827,#38828,#38829,#38830,#38831,#38832,#38833,#38834,#38835,
#38836),.UNSPECIFIED.,.F.,.F.,(4,3,3,3,3,3,3,3,3,3,3,3,3,3,3,3,3,3,3,3,
4),(-0.410648750432938,-0.381294613665594,-0.352267124576947,-0.328792823836752,
-0.311187098281605,-0.306018425011984,-0.301691296836585,-0.274143229574461,
-0.258369921616165,-0.230117472373342,-0.201352788326674,-0.195525900786732,
-0.16833922287309,-0.141249160586392,-0.114615533759621,-0.100282139063474,
-0.0960342097686789,-0.0702554174629941,-0.0448546715641945,-0.0201984500449382,
0.),.UNSPECIFIED.);
#2746=B_SPLINE_CURVE_WITH_KNOTS('',3,(#38839,#38840,#38841,#38842,#38843,
#38844,#38845,#38846,#38847,#38848,#38849,#38850,#38851,#38852,#38853,#38854,
#38855,#38856,#38857,#38858,#38859,#38860,#38861,#38862,#38863,#38864,#38865,
#38866,#38867,#38868,#38869),.UNSPECIFIED.,.F.,.F.,(4,3,3,3,3,3,3,3,3,3,
4),(-0.219677966288006,-0.206985183547511,-0.178213580556878,-0.148819200354015,
-0.130216800309763,-0.118450459252591,-0.113866160083042,-0.0841488051349767,
-0.0540951018364117,-0.0242019686830237,0.),.UNSPECIFIED.);
#2747=B_SPLINE_CURVE_WITH_KNOTS('',3,(#39182,#39183,#39184,#39185,#39186,
#39187,#39188,#39189),.UNSPECIFIED.,.F.,.F.,(4,1,1,1,1,4),(11.6150328478182,
12.6023632471184,13.5896936464185,14.5770240457187,15.5643544450188,15.7079632679489),
 .UNSPECIFIED.);
#2748=B_SPLINE_CURVE_WITH_KNOTS('',3,(#39190,#39191,#39192,#39193,#39194,
#39195,#39196,#39197,#39198,#39199,#39200,#39201,#39202,#39203,#39204,#39205,
#39206,#39207,#39208,#39209,#39210,#39211,#39212,#39213,#39214,#39215,#39216,
#39217,#39218,#39219,#39220,#39221,#39222,#39223,#39224,#39225,#39226,#39227,
#39228,#39229,#39230,#39231,#39232,#39233,#39234,#39235,#39236,#39237,#39238,
#39239,#39240,#39241,#39242,#39243,#39244,#39245,#39246,#39247,#39248,#39249,
#39250,#39251,#39252,#39253,#39254,#39255,#39256,#39257,#39258,#39259,#39260,
#39261,#39262,#39263,#39264,#39265,#39266,#39267,#39268,#39269,#39270,#39271,
#39272,#39273,#39274,#39275,#39276,#39277),.UNSPECIFIED.,.F.,.F.,(4,3,3,
3,3,3,3,3,3,3,3,3,3,3,3,3,3,3,3,3,3,3,3,3,3,3,3,3,3,4),(-0.55274537837504,
-0.525174630400016,-0.495740003900857,-0.479498227927527,-0.472105972866577,
-0.443064611280178,-0.418881458903182,-0.408301329738247,-0.401969450637142,
-0.397429868442983,-0.369124488132221,-0.341064938672273,-0.313899750226951,
-0.29772704364586,-0.291366968188088,-0.264559598151202,-0.249599392264211,
-0.222215347947115,-0.194438429453726,-0.189292991414398,-0.162670593649827,
-0.136062352557756,-0.109859916217256,-0.101879142728474,-0.0950850259724172,
-0.09115324392662,-0.0655931049079899,-0.0404250325776628,-0.0160423336449029,
0.),.UNSPECIFIED.);
#2749=B_SPLINE_CURVE_WITH_KNOTS('',3,(#39278,#39279,#39280,#39281,#39282,
#39283,#39284,#39285,#39286,#39287,#39288,#39289,#39290,#39291,#39292,#39293,
#39294,#39295,#39296),.UNSPECIFIED.,.F.,.F.,(4,3,3,3,3,3,4),(-71.548101301701,
-71.0877887496107,-70.1004583503106,-69.1131279510104,-68.1257975517103,
-67.1384671524101,-66.9247834919266),.UNSPECIFIED.);
#2750=B_SPLINE_CURVE_WITH_KNOTS('',3,(#39299,#39300,#39301,#39302,#39303,
#39304,#39305,#39306,#39307),.UNSPECIFIED.,.F.,.F.,(4,1,1,1,1,1,4),(10.3761157273102,
11.2731783835768,12.2617453273021,13.2503122710274,14.2388792147526,15.2274461584779,
15.7079632679489),.UNSPECIFIED.);
#2751=B_SPLINE_CURVE_WITH_KNOTS('',3,(#39625,#39626,#39627,#39628,#39629,
#39630,#39631,#39632,#39633,#39634,#39635,#39636,#39637,#39638,#39639,#39640,
#39641,#39642,#39643,#39644,#39645,#39646),.UNSPECIFIED.,.F.,.F.,(4,3,3,
3,3,3,3,4),(63.9491534801641,64.2568513421422,65.2454182858675,66.2339852295928,
67.222552173318,68.2111191170433,69.1996860607685,69.4794631267919),
 .UNSPECIFIED.);
#2752=B_SPLINE_CURVE_WITH_KNOTS('',3,(#39647,#39648,#39649,#39650,#39651,
#39652,#39653,#39654,#39655,#39656,#39657,#39658,#39659,#39660,#39661,#39662,
#39663,#39664,#39665,#39666,#39667,#39668,#39669,#39670,#39671,#39672,#39673,
#39674,#39675,#39676,#39677,#39678,#39679,#39680,#39681,#39682,#39683,#39684,
#39685,#39686,#39687,#39688,#39689,#39690,#39691,#39692,#39693,#39694,#39695,
#39696,#39697,#39698,#39699,#39700,#39701,#39702,#39703,#39704,#39705,#39706,
#39707,#39708,#39709,#39710,#39711,#39712,#39713,#39714,#39715,#39716,#39717,
#39718,#39719,#39720,#39721,#39722,#39723,#39724,#39725,#39726,#39727,#39728,
#39729,#39730,#39731,#39732,#39733,#39734),.UNSPECIFIED.,.F.,.F.,(4,3,3,
3,3,3,3,3,3,3,3,3,3,3,3,3,3,3,3,3,3,3,3,3,3,3,3,3,3,4),(-0.555272788399385,
-0.533197712400843,-0.50841200558917,-0.492097097422296,-0.487698425831477,
-0.461722637175749,-0.438993822101987,-0.427671428401512,-0.42202191869945,
-0.395458071621424,-0.368431943977533,-0.346296987129563,-0.329695769493585,
-0.32517826205158,-0.321068892319616,-0.293156561268766,-0.279892116585652,
-0.25291117159626,-0.225403496298925,-0.221057334466692,-0.216708298034074,
-0.188764735094145,-0.160284152968102,-0.131561788206246,-0.114355289595352,
-0.109564750157472,-0.0800994390258527,-0.050557237845911,-0.0215776241374192,
0.),.UNSPECIFIED.);
#3265=LINE('',#37765,#3803);
#3266=LINE('',#37789,#3804);
#3267=LINE('',#37837,#3805);
#3268=LINE('',#37885,#3806);
#3269=LINE('',#37939,#3807);
#3270=LINE('',#37987,#3808);
#3271=LINE('',#38035,#3809);
#3272=LINE('',#38089,#3810);
#3273=LINE('',#38137,#3811);
#3274=LINE('',#38188,#3812);
#3275=LINE('',#38239,#3813);
#3276=LINE('',#38287,#3814);
#3277=LINE('',#38312,#3815);
#3278=LINE('',#38337,#3816);
#3279=LINE('',#38361,#3817);
#3280=LINE('',#38387,#3818);
#3281=LINE('',#38411,#3819);
#3282=LINE('',#38436,#3820);
#3283=LINE('',#38461,#3821);
#3284=LINE('',#38485,#3822);
#3285=LINE('',#38510,#3823);
#3286=LINE('',#38535,#3824);
#3287=LINE('',#38871,#3825);
#3288=LINE('',#39739,#3826);
#3289=LINE('',#39741,#3827);
#3290=LINE('',#39743,#3828);
#3291=LINE('',#39744,#3829);
#3292=LINE('',#39747,#3830);
#3293=LINE('',#39749,#3831);
#3294=LINE('',#39750,#3832);
#3295=LINE('',#39753,#3833);
#3296=LINE('',#39755,#3834);
#3297=LINE('',#39756,#3835);
#3298=LINE('',#39759,#3836);
#3299=LINE('',#39761,#3837);
#3300=LINE('',#39762,#3838);
#3301=LINE('',#39765,#3839);
#3302=LINE('',#39767,#3840);
#3303=LINE('',#39768,#3841);
#3304=LINE('',#39770,#3842);
#3305=LINE('',#39771,#3843);
#3306=LINE('',#39778,#3844);
#3803=VECTOR('',#12998,3.);
#3804=VECTOR('',#13003,3.);
#3805=VECTOR('',#13006,3.);
#3806=VECTOR('',#13009,3.);
#3807=VECTOR('',#13012,3.);
#3808=VECTOR('',#13015,3.);
#3809=VECTOR('',#13018,3.);
#3810=VECTOR('',#13021,3.);
#3811=VECTOR('',#13024,3.);
#3812=VECTOR('',#13027,3.);
#3813=VECTOR('',#13030,3.);
#3814=VECTOR('',#13033,2.37175);
#3815=VECTOR('',#13038,2.37175);
#3816=VECTOR('',#13041,2.37175);
#3817=VECTOR('',#13044,2.37175);
#3818=VECTOR('',#13047,2.37175);
#3819=VECTOR('',#13050,2.37175);
#3820=VECTOR('',#13053,2.37175);
#3821=VECTOR('',#13056,2.37175);
#3822=VECTOR('',#13059,2.37175);
#3823=VECTOR('',#13062,2.37175);
#3824=VECTOR('',#13065,2.37175);
#3825=VECTOR('',#13070,2.5);
#3826=VECTOR('',#13081,10.);
#3827=VECTOR('',#13082,10.);
#3828=VECTOR('',#13083,10.);
#3829=VECTOR('',#13084,10.);
#3830=VECTOR('',#13087,10.);
#3831=VECTOR('',#13088,10.);
#3832=VECTOR('',#13089,10.);
#3833=VECTOR('',#13092,10.);
#3834=VECTOR('',#13093,10.);
#3835=VECTOR('',#13094,10.);
#3836=VECTOR('',#13097,10.);
#3837=VECTOR('',#13098,10.);
#3838=VECTOR('',#13099,10.);
#3839=VECTOR('',#13102,10.);
#3840=VECTOR('',#13103,10.);
#3841=VECTOR('',#13104,10.);
#3842=VECTOR('',#13107,10.);
#3843=VECTOR('',#13108,10.);
#3844=VECTOR('',#13117,5.);
#4741=VERTEX_POINT('',#37763);
#4742=VERTEX_POINT('',#37764);
#4743=VERTEX_POINT('',#37766);
#4744=VERTEX_POINT('',#37777);
#4745=VERTEX_POINT('',#37787);
#4746=VERTEX_POINT('',#37788);
#4747=VERTEX_POINT('',#37835);
#4748=VERTEX_POINT('',#37836);
#4749=VERTEX_POINT('',#37883);
#4750=VERTEX_POINT('',#37884);
#4751=VERTEX_POINT('',#37937);
#4752=VERTEX_POINT('',#37938);
#4753=VERTEX_POINT('',#37985);
#4754=VERTEX_POINT('',#37986);
#4755=VERTEX_POINT('',#38033);
#4756=VERTEX_POINT('',#38034);
#4757=VERTEX_POINT('',#38087);
#4758=VERTEX_POINT('',#38088);
#4759=VERTEX_POINT('',#38135);
#4760=VERTEX_POINT('',#38136);
#4761=VERTEX_POINT('',#38186);
#4762=VERTEX_POINT('',#38187);
#4763=VERTEX_POINT('',#38237);
#4764=VERTEX_POINT('',#38238);
#4765=VERTEX_POINT('',#38285);
#4766=VERTEX_POINT('',#38286);
#4767=VERTEX_POINT('',#38288);
#4768=VERTEX_POINT('',#38299);
#4769=VERTEX_POINT('',#38310);
#4770=VERTEX_POINT('',#38311);
#4771=VERTEX_POINT('',#38335);
#4772=VERTEX_POINT('',#38336);
#4773=VERTEX_POINT('',#38359);
#4774=VERTEX_POINT('',#38360);
#4775=VERTEX_POINT('',#38385);
#4776=VERTEX_POINT('',#38386);
#4777=VERTEX_POINT('',#38409);
#4778=VERTEX_POINT('',#38410);
#4779=VERTEX_POINT('',#38434);
#4780=VERTEX_POINT('',#38435);
#4781=VERTEX_POINT('',#38459);
#4782=VERTEX_POINT('',#38460);
#4783=VERTEX_POINT('',#38483);
#4784=VERTEX_POINT('',#38484);
#4785=VERTEX_POINT('',#38508);
#4786=VERTEX_POINT('',#38509);
#4787=VERTEX_POINT('',#38533);
#4788=VERTEX_POINT('',#38534);
#4789=VERTEX_POINT('',#38557);
#4790=VERTEX_POINT('',#38775);
#4791=VERTEX_POINT('',#38837);
#4792=VERTEX_POINT('',#38870);
#4793=VERTEX_POINT('',#39181);
#4794=VERTEX_POINT('',#39298);
#4795=VERTEX_POINT('',#39737);
#4796=VERTEX_POINT('',#39738);
#4797=VERTEX_POINT('',#39740);
#4798=VERTEX_POINT('',#39742);
#4799=VERTEX_POINT('',#39746);
#4800=VERTEX_POINT('',#39748);
#4801=VERTEX_POINT('',#39752);
#4802=VERTEX_POINT('',#39754);
#4803=VERTEX_POINT('',#39758);
#4804=VERTEX_POINT('',#39760);
#4805=VERTEX_POINT('',#39764);
#4806=VERTEX_POINT('',#39766);
#4807=VERTEX_POINT('',#39774);
#4808=VERTEX_POINT('',#39777);
#6185=EDGE_CURVE('',#4741,#4742,#3265,.T.);
#6186=EDGE_CURVE('',#4741,#4743,#2700,.T.);
#6187=EDGE_CURVE('',#4743,#4744,#1988,.F.);
#6188=EDGE_CURVE('',#4744,#4742,#2701,.T.);
#6189=EDGE_CURVE('',#4745,#4746,#3266,.T.);
#6190=EDGE_CURVE('',#4745,#4741,#2702,.T.);
#6191=EDGE_CURVE('',#4742,#4746,#2703,.T.);
#6192=EDGE_CURVE('',#4747,#4748,#3267,.T.);
#6193=EDGE_CURVE('',#4747,#4745,#2704,.T.);
#6194=EDGE_CURVE('',#4746,#4748,#2705,.T.);
#6195=EDGE_CURVE('',#4749,#4750,#3268,.T.);
#6196=EDGE_CURVE('',#4749,#4747,#2706,.T.);
#6197=EDGE_CURVE('',#4748,#4750,#2707,.T.);
#6198=EDGE_CURVE('',#4751,#4752,#3269,.T.);
#6199=EDGE_CURVE('',#4751,#4749,#2708,.T.);
#6200=EDGE_CURVE('',#4750,#4752,#2709,.T.);
#6201=EDGE_CURVE('',#4753,#4754,#3270,.T.);
#6202=EDGE_CURVE('',#4753,#4751,#2710,.T.);
#6203=EDGE_CURVE('',#4752,#4754,#2711,.T.);
#6204=EDGE_CURVE('',#4755,#4756,#3271,.T.);
#6205=EDGE_CURVE('',#4755,#4753,#2712,.T.);
#6206=EDGE_CURVE('',#4754,#4756,#2713,.T.);
#6207=EDGE_CURVE('',#4757,#4758,#3272,.T.);
#6208=EDGE_CURVE('',#4757,#4755,#2714,.T.);
#6209=EDGE_CURVE('',#4756,#4758,#2715,.T.);
#6210=EDGE_CURVE('',#4759,#4760,#3273,.T.);
#6211=EDGE_CURVE('',#4759,#4757,#2716,.T.);
#6212=EDGE_CURVE('',#4758,#4760,#2717,.T.);
#6213=EDGE_CURVE('',#4761,#4762,#3274,.T.);
#6214=EDGE_CURVE('',#4761,#4759,#2718,.T.);
#6215=EDGE_CURVE('',#4760,#4762,#2719,.T.);
#6216=EDGE_CURVE('',#4763,#4764,#3275,.T.);
#6217=EDGE_CURVE('',#4763,#4761,#2720,.T.);
#6218=EDGE_CURVE('',#4762,#4764,#2721,.T.);
#6219=EDGE_CURVE('',#4765,#4766,#3276,.T.);
#6220=EDGE_CURVE('',#4765,#4767,#2722,.T.);
#6221=EDGE_CURVE('',#4767,#4768,#1989,.T.);
#6222=EDGE_CURVE('',#4766,#4768,#2723,.T.);
#6223=EDGE_CURVE('',#4769,#4770,#3277,.T.);
#6224=EDGE_CURVE('',#4769,#4765,#2724,.T.);
#6225=EDGE_CURVE('',#4770,#4766,#2725,.T.);
#6226=EDGE_CURVE('',#4771,#4772,#3278,.T.);
#6227=EDGE_CURVE('',#4771,#4769,#2726,.T.);
#6228=EDGE_CURVE('',#4772,#4770,#2727,.T.);
#6229=EDGE_CURVE('',#4773,#4774,#3279,.T.);
#6230=EDGE_CURVE('',#4773,#4771,#2728,.T.);
#6231=EDGE_CURVE('',#4774,#4772,#2729,.T.);
#6232=EDGE_CURVE('',#4775,#4776,#3280,.T.);
#6233=EDGE_CURVE('',#4775,#4773,#2730,.T.);
#6234=EDGE_CURVE('',#4776,#4774,#2731,.T.);
#6235=EDGE_CURVE('',#4777,#4778,#3281,.T.);
#6236=EDGE_CURVE('',#4777,#4775,#2732,.T.);
#6237=EDGE_CURVE('',#4778,#4776,#2733,.T.);
#6238=EDGE_CURVE('',#4779,#4780,#3282,.T.);
#6239=EDGE_CURVE('',#4779,#4777,#2734,.T.);
#6240=EDGE_CURVE('',#4780,#4778,#2735,.T.);
#6241=EDGE_CURVE('',#4781,#4782,#3283,.T.);
#6242=EDGE_CURVE('',#4781,#4779,#2736,.T.);
#6243=EDGE_CURVE('',#4782,#4780,#2737,.T.);
#6244=EDGE_CURVE('',#4783,#4784,#3284,.T.);
#6245=EDGE_CURVE('',#4783,#4781,#2738,.T.);
#6246=EDGE_CURVE('',#4784,#4782,#2739,.T.);
#6247=EDGE_CURVE('',#4785,#4786,#3285,.T.);
#6248=EDGE_CURVE('',#4785,#4783,#2740,.T.);
#6249=EDGE_CURVE('',#4786,#4784,#2741,.T.);
#6250=EDGE_CURVE('',#4787,#4788,#3286,.T.);
#6251=EDGE_CURVE('',#4787,#4785,#2742,.T.);
#6252=EDGE_CURVE('',#4788,#4786,#2743,.T.);
#6253=EDGE_CURVE('',#4768,#4789,#2744,.T.);
#6254=EDGE_CURVE('',#4790,#4767,#2745,.T.);
#6255=EDGE_CURVE('',#4791,#4790,#1990,.T.);
#6256=EDGE_CURVE('',#4789,#4791,#2746,.T.);
#6257=EDGE_CURVE('',#4789,#4792,#3287,.T.);
#6258=EDGE_CURVE('',#4792,#4792,#1991,.T.);
#6259=EDGE_CURVE('',#4793,#4787,#2747,.T.);
#6260=EDGE_CURVE('',#4743,#4793,#2748,.T.);
#6261=EDGE_CURVE('',#4790,#4763,#2749,.T.);
#6262=EDGE_CURVE('',#4794,#4788,#2750,.T.);
#6263=EDGE_CURVE('',#4793,#4794,#1992,.T.);
#6264=EDGE_CURVE('',#4764,#4791,#2751,.T.);
#6265=EDGE_CURVE('',#4794,#4744,#2752,.T.);
#6266=EDGE_CURVE('',#4795,#4796,#3288,.T.);
#6267=EDGE_CURVE('',#4795,#4797,#3289,.T.);
#6268=EDGE_CURVE('',#4797,#4798,#3290,.T.);
#6269=EDGE_CURVE('',#4796,#4798,#3291,.T.);
#6270=EDGE_CURVE('',#4799,#4795,#3292,.T.);
#6271=EDGE_CURVE('',#4799,#4800,#3293,.T.);
#6272=EDGE_CURVE('',#4800,#4797,#3294,.T.);
#6273=EDGE_CURVE('',#4801,#4799,#3295,.T.);
#6274=EDGE_CURVE('',#4801,#4802,#3296,.T.);
#6275=EDGE_CURVE('',#4802,#4800,#3297,.T.);
#6276=EDGE_CURVE('',#4803,#4801,#3298,.T.);
#6277=EDGE_CURVE('',#4803,#4804,#3299,.T.);
#6278=EDGE_CURVE('',#4804,#4802,#3300,.T.);
#6279=EDGE_CURVE('',#4805,#4803,#3301,.T.);
#6280=EDGE_CURVE('',#4805,#4806,#3302,.T.);
#6281=EDGE_CURVE('',#4806,#4804,#3303,.T.);
#6282=EDGE_CURVE('',#4796,#4805,#3304,.T.);
#6283=EDGE_CURVE('',#4798,#4806,#3305,.T.);
#6284=EDGE_CURVE('',#4807,#4807,#1993,.T.);
#6285=EDGE_CURVE('',#4807,#4808,#3306,.T.);
#6286=EDGE_CURVE('',#4808,#4808,#1994,.T.);
#9005=ORIENTED_EDGE('',*,*,#6185,.F.);
#9006=ORIENTED_EDGE('',*,*,#6186,.T.);
#9007=ORIENTED_EDGE('',*,*,#6187,.T.);
#9008=ORIENTED_EDGE('',*,*,#6188,.T.);
#9009=ORIENTED_EDGE('',*,*,#6189,.F.);
#9010=ORIENTED_EDGE('',*,*,#6190,.T.);
#9011=ORIENTED_EDGE('',*,*,#6185,.T.);
#9012=ORIENTED_EDGE('',*,*,#6191,.T.);
#9013=ORIENTED_EDGE('',*,*,#6192,.F.);
#9014=ORIENTED_EDGE('',*,*,#6193,.T.);
#9015=ORIENTED_EDGE('',*,*,#6189,.T.);
#9016=ORIENTED_EDGE('',*,*,#6194,.T.);
#9017=ORIENTED_EDGE('',*,*,#6195,.F.);
#9018=ORIENTED_EDGE('',*,*,#6196,.T.);
#9019=ORIENTED_EDGE('',*,*,#6192,.T.);
#9020=ORIENTED_EDGE('',*,*,#6197,.T.);
#9021=ORIENTED_EDGE('',*,*,#6198,.F.);
#9022=ORIENTED_EDGE('',*,*,#6199,.T.);
#9023=ORIENTED_EDGE('',*,*,#6195,.T.);
#9024=ORIENTED_EDGE('',*,*,#6200,.T.);
#9025=ORIENTED_EDGE('',*,*,#6201,.F.);
#9026=ORIENTED_EDGE('',*,*,#6202,.T.);
#9027=ORIENTED_EDGE('',*,*,#6198,.T.);
#9028=ORIENTED_EDGE('',*,*,#6203,.T.);
#9029=ORIENTED_EDGE('',*,*,#6204,.F.);
#9030=ORIENTED_EDGE('',*,*,#6205,.T.);
#9031=ORIENTED_EDGE('',*,*,#6201,.T.);
#9032=ORIENTED_EDGE('',*,*,#6206,.T.);
#9033=ORIENTED_EDGE('',*,*,#6207,.F.);
#9034=ORIENTED_EDGE('',*,*,#6208,.T.);
#9035=ORIENTED_EDGE('',*,*,#6204,.T.);
#9036=ORIENTED_EDGE('',*,*,#6209,.T.);
#9037=ORIENTED_EDGE('',*,*,#6210,.F.);
#9038=ORIENTED_EDGE('',*,*,#6211,.T.);
#9039=ORIENTED_EDGE('',*,*,#6207,.T.);
#9040=ORIENTED_EDGE('',*,*,#6212,.T.);
#9041=ORIENTED_EDGE('',*,*,#6213,.F.);
#9042=ORIENTED_EDGE('',*,*,#6214,.T.);
#9043=ORIENTED_EDGE('',*,*,#6210,.T.);
#9044=ORIENTED_EDGE('',*,*,#6215,.T.);
#9045=ORIENTED_EDGE('',*,*,#6216,.F.);
#9046=ORIENTED_EDGE('',*,*,#6217,.T.);
#9047=ORIENTED_EDGE('',*,*,#6213,.T.);
#9048=ORIENTED_EDGE('',*,*,#6218,.T.);
#9049=ORIENTED_EDGE('',*,*,#6219,.F.);
#9050=ORIENTED_EDGE('',*,*,#6220,.T.);
#9051=ORIENTED_EDGE('',*,*,#6221,.T.);
#9052=ORIENTED_EDGE('',*,*,#6222,.F.);
#9053=ORIENTED_EDGE('',*,*,#6223,.F.);
#9054=ORIENTED_EDGE('',*,*,#6224,.T.);
#9055=ORIENTED_EDGE('',*,*,#6219,.T.);
#9056=ORIENTED_EDGE('',*,*,#6225,.F.);
#9057=ORIENTED_EDGE('',*,*,#6226,.F.);
#9058=ORIENTED_EDGE('',*,*,#6227,.T.);
#9059=ORIENTED_EDGE('',*,*,#6223,.T.);
#9060=ORIENTED_EDGE('',*,*,#6228,.F.);
#9061=ORIENTED_EDGE('',*,*,#6229,.F.);
#9062=ORIENTED_EDGE('',*,*,#6230,.T.);
#9063=ORIENTED_EDGE('',*,*,#6226,.T.);
#9064=ORIENTED_EDGE('',*,*,#6231,.F.);
#9065=ORIENTED_EDGE('',*,*,#6232,.F.);
#9066=ORIENTED_EDGE('',*,*,#6233,.T.);
#9067=ORIENTED_EDGE('',*,*,#6229,.T.);
#9068=ORIENTED_EDGE('',*,*,#6234,.F.);
#9069=ORIENTED_EDGE('',*,*,#6235,.F.);
#9070=ORIENTED_EDGE('',*,*,#6236,.T.);
#9071=ORIENTED_EDGE('',*,*,#6232,.T.);
#9072=ORIENTED_EDGE('',*,*,#6237,.F.);
#9073=ORIENTED_EDGE('',*,*,#6238,.F.);
#9074=ORIENTED_EDGE('',*,*,#6239,.T.);
#9075=ORIENTED_EDGE('',*,*,#6235,.T.);
#9076=ORIENTED_EDGE('',*,*,#6240,.F.);
#9077=ORIENTED_EDGE('',*,*,#6241,.F.);
#9078=ORIENTED_EDGE('',*,*,#6242,.T.);
#9079=ORIENTED_EDGE('',*,*,#6238,.T.);
#9080=ORIENTED_EDGE('',*,*,#6243,.F.);
#9081=ORIENTED_EDGE('',*,*,#6244,.F.);
#9082=ORIENTED_EDGE('',*,*,#6245,.T.);
#9083=ORIENTED_EDGE('',*,*,#6241,.T.);
#9084=ORIENTED_EDGE('',*,*,#6246,.F.);
#9085=ORIENTED_EDGE('',*,*,#6247,.F.);
#9086=ORIENTED_EDGE('',*,*,#6248,.T.);
#9087=ORIENTED_EDGE('',*,*,#6244,.T.);
#9088=ORIENTED_EDGE('',*,*,#6249,.F.);
#9089=ORIENTED_EDGE('',*,*,#6250,.F.);
#9090=ORIENTED_EDGE('',*,*,#6251,.T.);
#9091=ORIENTED_EDGE('',*,*,#6247,.T.);
#9092=ORIENTED_EDGE('',*,*,#6252,.F.);
#9093=ORIENTED_EDGE('',*,*,#6253,.F.);
#9094=ORIENTED_EDGE('',*,*,#6221,.F.);
#9095=ORIENTED_EDGE('',*,*,#6254,.F.);
#9096=ORIENTED_EDGE('',*,*,#6255,.F.);
#9097=ORIENTED_EDGE('',*,*,#6256,.F.);
#9098=ORIENTED_EDGE('',*,*,#6257,.T.);
#9099=ORIENTED_EDGE('',*,*,#6258,.F.);
#9100=ORIENTED_EDGE('',*,*,#6257,.F.);
#9101=ORIENTED_EDGE('',*,*,#6254,.T.);
#9102=ORIENTED_EDGE('',*,*,#6220,.F.);
#9103=ORIENTED_EDGE('',*,*,#6224,.F.);
#9104=ORIENTED_EDGE('',*,*,#6227,.F.);
#9105=ORIENTED_EDGE('',*,*,#6230,.F.);
#9106=ORIENTED_EDGE('',*,*,#6233,.F.);
#9107=ORIENTED_EDGE('',*,*,#6236,.F.);
#9108=ORIENTED_EDGE('',*,*,#6239,.F.);
#9109=ORIENTED_EDGE('',*,*,#6242,.F.);
#9110=ORIENTED_EDGE('',*,*,#6245,.F.);
#9111=ORIENTED_EDGE('',*,*,#6248,.F.);
#9112=ORIENTED_EDGE('',*,*,#6251,.F.);
#9113=ORIENTED_EDGE('',*,*,#6259,.F.);
#9114=ORIENTED_EDGE('',*,*,#6260,.F.);
#9115=ORIENTED_EDGE('',*,*,#6186,.F.);
#9116=ORIENTED_EDGE('',*,*,#6190,.F.);
#9117=ORIENTED_EDGE('',*,*,#6193,.F.);
#9118=ORIENTED_EDGE('',*,*,#6196,.F.);
#9119=ORIENTED_EDGE('',*,*,#6199,.F.);
#9120=ORIENTED_EDGE('',*,*,#6202,.F.);
#9121=ORIENTED_EDGE('',*,*,#6205,.F.);
#9122=ORIENTED_EDGE('',*,*,#6208,.F.);
#9123=ORIENTED_EDGE('',*,*,#6211,.F.);
#9124=ORIENTED_EDGE('',*,*,#6214,.F.);
#9125=ORIENTED_EDGE('',*,*,#6217,.F.);
#9126=ORIENTED_EDGE('',*,*,#6261,.F.);
#9127=ORIENTED_EDGE('',*,*,#6250,.T.);
#9128=ORIENTED_EDGE('',*,*,#6262,.F.);
#9129=ORIENTED_EDGE('',*,*,#6263,.F.);
#9130=ORIENTED_EDGE('',*,*,#6259,.T.);
#9131=ORIENTED_EDGE('',*,*,#6253,.T.);
#9132=ORIENTED_EDGE('',*,*,#6256,.T.);
#9133=ORIENTED_EDGE('',*,*,#6264,.F.);
#9134=ORIENTED_EDGE('',*,*,#6218,.F.);
#9135=ORIENTED_EDGE('',*,*,#6215,.F.);
#9136=ORIENTED_EDGE('',*,*,#6212,.F.);
#9137=ORIENTED_EDGE('',*,*,#6209,.F.);
#9138=ORIENTED_EDGE('',*,*,#6206,.F.);
#9139=ORIENTED_EDGE('',*,*,#6203,.F.);
#9140=ORIENTED_EDGE('',*,*,#6200,.F.);
#9141=ORIENTED_EDGE('',*,*,#6197,.F.);
#9142=ORIENTED_EDGE('',*,*,#6194,.F.);
#9143=ORIENTED_EDGE('',*,*,#6191,.F.);
#9144=ORIENTED_EDGE('',*,*,#6188,.F.);
#9145=ORIENTED_EDGE('',*,*,#6265,.F.);
#9146=ORIENTED_EDGE('',*,*,#6262,.T.);
#9147=ORIENTED_EDGE('',*,*,#6252,.T.);
#9148=ORIENTED_EDGE('',*,*,#6249,.T.);
#9149=ORIENTED_EDGE('',*,*,#6246,.T.);
#9150=ORIENTED_EDGE('',*,*,#6243,.T.);
#9151=ORIENTED_EDGE('',*,*,#6240,.T.);
#9152=ORIENTED_EDGE('',*,*,#6237,.T.);
#9153=ORIENTED_EDGE('',*,*,#6234,.T.);
#9154=ORIENTED_EDGE('',*,*,#6231,.T.);
#9155=ORIENTED_EDGE('',*,*,#6228,.T.);
#9156=ORIENTED_EDGE('',*,*,#6225,.T.);
#9157=ORIENTED_EDGE('',*,*,#6222,.T.);
#9158=ORIENTED_EDGE('',*,*,#6216,.T.);
#9159=ORIENTED_EDGE('',*,*,#6264,.T.);
#9160=ORIENTED_EDGE('',*,*,#6255,.T.);
#9161=ORIENTED_EDGE('',*,*,#6261,.T.);
#9162=ORIENTED_EDGE('',*,*,#6266,.F.);
#9163=ORIENTED_EDGE('',*,*,#6267,.T.);
#9164=ORIENTED_EDGE('',*,*,#6268,.T.);
#9165=ORIENTED_EDGE('',*,*,#6269,.F.);
#9166=ORIENTED_EDGE('',*,*,#6270,.F.);
#9167=ORIENTED_EDGE('',*,*,#6271,.T.);
#9168=ORIENTED_EDGE('',*,*,#6272,.T.);
#9169=ORIENTED_EDGE('',*,*,#6267,.F.);
#9170=ORIENTED_EDGE('',*,*,#6273,.F.);
#9171=ORIENTED_EDGE('',*,*,#6274,.T.);
#9172=ORIENTED_EDGE('',*,*,#6275,.T.);
#9173=ORIENTED_EDGE('',*,*,#6271,.F.);
#9174=ORIENTED_EDGE('',*,*,#6276,.F.);
#9175=ORIENTED_EDGE('',*,*,#6277,.T.);
#9176=ORIENTED_EDGE('',*,*,#6278,.T.);
#9177=ORIENTED_EDGE('',*,*,#6274,.F.);
#9178=ORIENTED_EDGE('',*,*,#6279,.F.);
#9179=ORIENTED_EDGE('',*,*,#6280,.T.);
#9180=ORIENTED_EDGE('',*,*,#6281,.T.);
#9181=ORIENTED_EDGE('',*,*,#6277,.F.);
#9182=ORIENTED_EDGE('',*,*,#6282,.F.);
#9183=ORIENTED_EDGE('',*,*,#6269,.T.);
#9184=ORIENTED_EDGE('',*,*,#6283,.T.);
#9185=ORIENTED_EDGE('',*,*,#6280,.F.);
#9186=ORIENTED_EDGE('',*,*,#6283,.F.);
#9187=ORIENTED_EDGE('',*,*,#6268,.F.);
#9188=ORIENTED_EDGE('',*,*,#6272,.F.);
#9189=ORIENTED_EDGE('',*,*,#6275,.F.);
#9190=ORIENTED_EDGE('',*,*,#6278,.F.);
#9191=ORIENTED_EDGE('',*,*,#6281,.F.);
#9192=ORIENTED_EDGE('',*,*,#6284,.T.);
#9193=ORIENTED_EDGE('',*,*,#6260,.T.);
#9194=ORIENTED_EDGE('',*,*,#6263,.T.);
#9195=ORIENTED_EDGE('',*,*,#6265,.T.);
#9196=ORIENTED_EDGE('',*,*,#6187,.F.);
#9197=ORIENTED_EDGE('',*,*,#6284,.F.);
#9198=ORIENTED_EDGE('',*,*,#6285,.T.);
#9199=ORIENTED_EDGE('',*,*,#6286,.T.);
#9200=ORIENTED_EDGE('',*,*,#6285,.F.);
#9201=ORIENTED_EDGE('',*,*,#6286,.F.);
#9202=ORIENTED_EDGE('',*,*,#6266,.T.);
#9203=ORIENTED_EDGE('',*,*,#6282,.T.);
#9204=ORIENTED_EDGE('',*,*,#6279,.T.);
#9205=ORIENTED_EDGE('',*,*,#6276,.T.);
#9206=ORIENTED_EDGE('',*,*,#6273,.T.);
#9207=ORIENTED_EDGE('',*,*,#6270,.T.);
#9208=ORIENTED_EDGE('',*,*,#6258,.T.);
#9782=CYLINDRICAL_SURFACE('',#11116,2.942);
#9783=CYLINDRICAL_SURFACE('',#11118,2.942);
#9784=CYLINDRICAL_SURFACE('',#11119,2.942);
#9785=CYLINDRICAL_SURFACE('',#11120,2.942);
#9786=CYLINDRICAL_SURFACE('',#11121,2.942);
#9787=CYLINDRICAL_SURFACE('',#11122,2.942);
#9788=CYLINDRICAL_SURFACE('',#11123,2.942);
#9789=CYLINDRICAL_SURFACE('',#11124,2.942);
#9790=CYLINDRICAL_SURFACE('',#11125,2.942);
#9791=CYLINDRICAL_SURFACE('',#11126,2.942);
#9792=CYLINDRICAL_SURFACE('',#11127,2.942);
#9793=CYLINDRICAL_SURFACE('',#11128,2.37175);
#9794=CYLINDRICAL_SURFACE('',#11130,2.37175);
#9795=CYLINDRICAL_SURFACE('',#11131,2.37175);
#9796=CYLINDRICAL_SURFACE('',#11132,2.37175);
#9797=CYLINDRICAL_SURFACE('',#11133,2.37175);
#9798=CYLINDRICAL_SURFACE('',#11134,2.37175);
#9799=CYLINDRICAL_SURFACE('',#11135,2.37175);
#9800=CYLINDRICAL_SURFACE('',#11136,2.37175);
#9801=CYLINDRICAL_SURFACE('',#11137,2.37175);
#9802=CYLINDRICAL_SURFACE('',#11138,2.37175);
#9803=CYLINDRICAL_SURFACE('',#11139,2.37175);
#9804=CYLINDRICAL_SURFACE('',#11143,2.37175);
#9805=CYLINDRICAL_SURFACE('',#11145,2.942);
#9806=CYLINDRICAL_SURFACE('',#11155,5.);
#10299=ADVANCED_FACE('',(#1063),#9782,.T.);
#10300=ADVANCED_FACE('',(#1064),#9783,.T.);
#10301=ADVANCED_FACE('',(#1065),#9784,.T.);
#10302=ADVANCED_FACE('',(#1066),#9785,.T.);
#10303=ADVANCED_FACE('',(#1067),#9786,.T.);
#10304=ADVANCED_FACE('',(#1068),#9787,.T.);
#10305=ADVANCED_FACE('',(#1069),#9788,.T.);
#10306=ADVANCED_FACE('',(#1070),#9789,.T.);
#10307=ADVANCED_FACE('',(#1071),#9790,.T.);
#10308=ADVANCED_FACE('',(#1072),#9791,.T.);
#10309=ADVANCED_FACE('',(#1073),#9792,.T.);
#10310=ADVANCED_FACE('',(#1074),#9793,.T.);
#10311=ADVANCED_FACE('',(#1075),#9794,.T.);
#10312=ADVANCED_FACE('',(#1076),#9795,.T.);
#10313=ADVANCED_FACE('',(#1077),#9796,.T.);
#10314=ADVANCED_FACE('',(#1078),#9797,.T.);
#10315=ADVANCED_FACE('',(#1079),#9798,.T.);
#10316=ADVANCED_FACE('',(#1080),#9799,.T.);
#10317=ADVANCED_FACE('',(#1081),#9800,.T.);
#10318=ADVANCED_FACE('',(#1082),#9801,.T.);
#10319=ADVANCED_FACE('',(#1083),#9802,.T.);
#10320=ADVANCED_FACE('',(#1084),#9803,.T.);
#10321=ADVANCED_FACE('',(#1085),#312,.T.);
#10322=ADVANCED_FACE('',(#1086),#599,.F.);
#10323=ADVANCED_FACE('',(#1087),#9804,.T.);
#10324=ADVANCED_FACE('',(#1088),#600,.F.);
#10325=ADVANCED_FACE('',(#1089),#9805,.T.);
#10326=ADVANCED_FACE('',(#1090),#557,.F.);
#10327=ADVANCED_FACE('',(#1091),#558,.F.);
#10328=ADVANCED_FACE('',(#1092),#559,.F.);
#10329=ADVANCED_FACE('',(#1093),#560,.F.);
#10330=ADVANCED_FACE('',(#1094),#561,.F.);
#10331=ADVANCED_FACE('',(#1095),#562,.F.);
#10332=ADVANCED_FACE('',(#1096),#563,.F.);
#10333=ADVANCED_FACE('',(#1097,#473),#564,.T.);
#10334=ADVANCED_FACE('',(#1098),#9806,.T.);
#10335=ADVANCED_FACE('',(#1099,#474),#565,.F.);
#10336=ADVANCED_FACE('',(#1100),#566,.T.);
#10390=CLOSED_SHELL('',(#10299,#10300,#10301,#10302,#10303,#10304,#10305,
#10306,#10307,#10308,#10309,#10310,#10311,#10312,#10313,#10314,#10315,#10316,
#10317,#10318,#10319,#10320,#10321,#10322,#10323,#10324,#10325,#10326,#10327,
#10328,#10329,#10330,#10331,#10332,#10333,#10334,#10335,#10336));
#11115=AXIS2_PLACEMENT_3D('',#37761,#12994,#12995);
#11116=AXIS2_PLACEMENT_3D('',#37762,#12996,#12997);
#11117=AXIS2_PLACEMENT_3D('',#37778,#12999,#13000);
#11118=AXIS2_PLACEMENT_3D('',#37786,#13001,#13002);
#11119=AXIS2_PLACEMENT_3D('',#37834,#13004,#13005);
#11120=AXIS2_PLACEMENT_3D('',#37882,#13007,#13008);
#11121=AXIS2_PLACEMENT_3D('',#37936,#13010,#13011);
#11122=AXIS2_PLACEMENT_3D('',#37984,#13013,#13014);
#11123=AXIS2_PLACEMENT_3D('',#38032,#13016,#13017);
#11124=AXIS2_PLACEMENT_3D('',#38086,#13019,#13020);
#11125=AXIS2_PLACEMENT_3D('',#38134,#13022,#13023);
#11126=AXIS2_PLACEMENT_3D('',#38185,#13025,#13026);
#11127=AXIS2_PLACEMENT_3D('',#38236,#13028,#13029);
#11128=AXIS2_PLACEMENT_3D('',#38284,#13031,#13032);
#11129=AXIS2_PLACEMENT_3D('',#38300,#13034,#13035);
#11130=AXIS2_PLACEMENT_3D('',#38309,#13036,#13037);
#11131=AXIS2_PLACEMENT_3D('',#38334,#13039,#13040);
#11132=AXIS2_PLACEMENT_3D('',#38358,#13042,#13043);
#11133=AXIS2_PLACEMENT_3D('',#38384,#13045,#13046);
#11134=AXIS2_PLACEMENT_3D('',#38408,#13048,#13049);
#11135=AXIS2_PLACEMENT_3D('',#38433,#13051,#13052);
#11136=AXIS2_PLACEMENT_3D('',#38458,#13054,#13055);
#11137=AXIS2_PLACEMENT_3D('',#38482,#13057,#13058);
#11138=AXIS2_PLACEMENT_3D('',#38507,#13060,#13061);
#11139=AXIS2_PLACEMENT_3D('',#38532,#13063,#13064);
#11140=AXIS2_PLACEMENT_3D('',#38556,#13066,#13067);
#11141=AXIS2_PLACEMENT_3D('',#38838,#13068,#13069);
#11142=AXIS2_PLACEMENT_3D('',#38872,#13071,#13072);
#11143=AXIS2_PLACEMENT_3D('',#39297,#13073,#13074);
#11144=AXIS2_PLACEMENT_3D('',#39308,#13075,#13076);
#11145=AXIS2_PLACEMENT_3D('',#39735,#13077,#13078);
#11146=AXIS2_PLACEMENT_3D('',#39736,#13079,#13080);
#11147=AXIS2_PLACEMENT_3D('',#39745,#13085,#13086);
#11148=AXIS2_PLACEMENT_3D('',#39751,#13090,#13091);
#11149=AXIS2_PLACEMENT_3D('',#39757,#13095,#13096);
#11150=AXIS2_PLACEMENT_3D('',#39763,#13100,#13101);
#11151=AXIS2_PLACEMENT_3D('',#39769,#13105,#13106);
#11152=AXIS2_PLACEMENT_3D('',#39772,#13109,#13110);
#11153=AXIS2_PLACEMENT_3D('',#39773,#13111,#13112);
#11154=AXIS2_PLACEMENT_3D('',#39775,#13113,#13114);
#11155=AXIS2_PLACEMENT_3D('',#39776,#13115,#13116);
#11156=AXIS2_PLACEMENT_3D('',#39779,#13118,#13119);
#11157=AXIS2_PLACEMENT_3D('',#39780,#13120,#13121);
#11158=AXIS2_PLACEMENT_3D('',#39781,#13122,#13123);
#12994=DIRECTION('axis',(0.,0.,1.));
#12995=DIRECTION('refdir',(1.,0.,0.));
#12996=DIRECTION('center_axis',(0.,0.,1.));
#12997=DIRECTION('ref_axis',(1.,0.,0.));
#12998=DIRECTION('',(0.,0.,-1.));
#12999=DIRECTION('center_axis',(0.,0.,-1.));
#13000=DIRECTION('ref_axis',(1.,0.,0.));
#13001=DIRECTION('center_axis',(0.,0.,1.));
#13002=DIRECTION('ref_axis',(1.,0.,0.));
#13003=DIRECTION('',(0.,0.,-1.));
#13004=DIRECTION('center_axis',(0.,0.,1.));
#13005=DIRECTION('ref_axis',(1.,0.,0.));
#13006=DIRECTION('',(0.,0.,-1.));
#13007=DIRECTION('center_axis',(0.,0.,1.));
#13008=DIRECTION('ref_axis',(1.,0.,0.));
#13009=DIRECTION('',(0.,0.,-1.));
#13010=DIRECTION('center_axis',(0.,0.,1.));
#13011=DIRECTION('ref_axis',(1.,0.,0.));
#13012=DIRECTION('',(0.,0.,-1.));
#13013=DIRECTION('center_axis',(0.,0.,1.));
#13014=DIRECTION('ref_axis',(1.,0.,0.));
#13015=DIRECTION('',(0.,0.,-1.));
#13016=DIRECTION('center_axis',(0.,0.,1.));
#13017=DIRECTION('ref_axis',(1.,0.,0.));
#13018=DIRECTION('',(0.,0.,-1.));
#13019=DIRECTION('center_axis',(0.,0.,1.));
#13020=DIRECTION('ref_axis',(1.,0.,0.));
#13021=DIRECTION('',(0.,0.,-1.));
#13022=DIRECTION('center_axis',(0.,0.,1.));
#13023=DIRECTION('ref_axis',(1.,0.,0.));
#13024=DIRECTION('',(0.,0.,-1.));
#13025=DIRECTION('center_axis',(0.,0.,1.));
#13026=DIRECTION('ref_axis',(1.,0.,0.));
#13027=DIRECTION('',(0.,0.,-1.));
#13028=DIRECTION('center_axis',(0.,0.,1.));
#13029=DIRECTION('ref_axis',(1.,0.,0.));
#13030=DIRECTION('',(0.,0.,-1.));
#13031=DIRECTION('center_axis',(0.,0.,1.));
#13032=DIRECTION('ref_axis',(0.997344302588954,-0.0728309144069492,0.));
#13033=DIRECTION('',(0.,0.,1.));
#13034=DIRECTION('center_axis',(0.,0.,-1.));
#13035=DIRECTION('ref_axis',(1.,7.52212518638754E-14,0.));
#13036=DIRECTION('center_axis',(0.,0.,1.));
#13037=DIRECTION('ref_axis',(1.,7.52212518638754E-14,0.));
#13038=DIRECTION('',(0.,0.,1.));
#13039=DIRECTION('center_axis',(0.,0.,1.));
#13040=DIRECTION('ref_axis',(1.,7.52212518638754E-14,0.));
#13041=DIRECTION('',(0.,0.,1.));
#13042=DIRECTION('center_axis',(0.,0.,1.));
#13043=DIRECTION('ref_axis',(1.,7.52212518638754E-14,0.));
#13044=DIRECTION('',(0.,0.,1.));
#13045=DIRECTION('center_axis',(0.,0.,1.));
#13046=DIRECTION('ref_axis',(1.,7.52212518638754E-14,0.));
#13047=DIRECTION('',(0.,0.,1.));
#13048=DIRECTION('center_axis',(0.,0.,1.));
#13049=DIRECTION('ref_axis',(1.,7.52212518638754E-14,0.));
#13050=DIRECTION('',(0.,0.,1.));
#13051=DIRECTION('center_axis',(0.,0.,1.));
#13052=DIRECTION('ref_axis',(1.,7.52212518638754E-14,0.));
#13053=DIRECTION('',(0.,0.,1.));
#13054=DIRECTION('center_axis',(0.,0.,1.));
#13055=DIRECTION('ref_axis',(1.,7.52212518638754E-14,0.));
#13056=DIRECTION('',(0.,0.,1.));
#13057=DIRECTION('center_axis',(0.,0.,1.));
#13058=DIRECTION('ref_axis',(1.,7.52212518638754E-14,0.));
#13059=DIRECTION('',(0.,0.,1.));
#13060=DIRECTION('center_axis',(0.,0.,1.));
#13061=DIRECTION('ref_axis',(1.,7.52212518638754E-14,0.));
#13062=DIRECTION('',(0.,0.,1.));
#13063=DIRECTION('center_axis',(0.,0.,1.));
#13064=DIRECTION('ref_axis',(1.,7.52212518638754E-14,0.));
#13065=DIRECTION('',(0.,0.,1.));
#13066=DIRECTION('center_axis',(0.,0.,-1.));
#13067=DIRECTION('ref_axis',(1.,0.,0.));
#13068=DIRECTION('center_axis',(0.,0.,-1.));
#13069=DIRECTION('ref_axis',(1.,0.,0.));
#13070=DIRECTION('',(0.707106781186548,8.65956056235494E-17,0.707106781186547));
#13071=DIRECTION('center_axis',(0.,0.,1.));
#13072=DIRECTION('ref_axis',(1.,0.,0.));
#13073=DIRECTION('center_axis',(0.,0.,1.));
#13074=DIRECTION('ref_axis',(1.,7.52212518638754E-14,0.));
#13075=DIRECTION('center_axis',(0.,0.,-1.));
#13076=DIRECTION('ref_axis',(1.,7.52212518638754E-14,0.));
#13077=DIRECTION('center_axis',(0.,0.,1.));
#13078=DIRECTION('ref_axis',(1.,0.,0.));
#13079=DIRECTION('center_axis',(-1.92296268638356E-16,-1.,0.));
#13080=DIRECTION('ref_axis',(1.,-1.92296268638356E-16,0.));
#13081=DIRECTION('',(1.,-1.92296268638356E-16,0.));
#13082=DIRECTION('',(0.,0.,1.));
#13083=DIRECTION('',(1.,-1.92296268638356E-16,0.));
#13084=DIRECTION('',(0.,0.,1.));
#13085=DIRECTION('center_axis',(-0.866025403784439,-0.5,0.));
#13086=DIRECTION('ref_axis',(0.5,-0.866025403784439,0.));
#13087=DIRECTION('',(0.5,-0.866025403784439,0.));
#13088=DIRECTION('',(0.,0.,1.));
#13089=DIRECTION('',(0.5,-0.866025403784439,0.));
#13090=DIRECTION('center_axis',(-0.866025403784439,0.5,0.));
#13091=DIRECTION('ref_axis',(-0.5,-0.866025403784438,0.));
#13092=DIRECTION('',(-0.5,-0.866025403784438,0.));
#13093=DIRECTION('',(0.,0.,1.));
#13094=DIRECTION('',(-0.5,-0.866025403784439,0.));
#13095=DIRECTION('center_axis',(1.92296268638356E-16,1.,0.));
#13096=DIRECTION('ref_axis',(-1.,1.92296268638356E-16,0.));
#13097=DIRECTION('',(-1.,1.92296268638356E-16,0.));
#13098=DIRECTION('',(0.,0.,1.));
#13099=DIRECTION('',(-1.,1.92296268638356E-16,0.));
#13100=DIRECTION('center_axis',(0.866025403784439,0.5,0.));
#13101=DIRECTION('ref_axis',(-0.5,0.866025403784439,0.));
#13102=DIRECTION('',(-0.5,0.866025403784439,0.));
#13103=DIRECTION('',(0.,0.,1.));
#13104=DIRECTION('',(-0.5,0.866025403784439,0.));
#13105=DIRECTION('center_axis',(0.866025403784439,-0.5,0.));
#13106=DIRECTION('ref_axis',(0.5,0.866025403784439,0.));
#13107=DIRECTION('',(0.5,0.866025403784439,0.));
#13108=DIRECTION('',(0.5,0.866025403784439,0.));
#13109=DIRECTION('center_axis',(0.,0.,1.));
#13110=DIRECTION('ref_axis',(1.,0.,0.));
#13111=DIRECTION('center_axis',(0.,0.,1.));
#13112=DIRECTION('ref_axis',(1.,0.,0.));
#13113=DIRECTION('center_axis',(0.,0.,1.));
#13114=DIRECTION('ref_axis',(1.,0.,0.));
#13115=DIRECTION('center_axis',(0.,0.,1.));
#13116=DIRECTION('ref_axis',(1.,0.,0.));
#13117=DIRECTION('',(0.,0.,-1.));
#13118=DIRECTION('center_axis',(0.,0.,1.));
#13119=DIRECTION('ref_axis',(1.,0.,0.));
#13120=DIRECTION('center_axis',(0.,0.,1.));
#13121=DIRECTION('ref_axis',(1.,0.,0.));
#13122=DIRECTION('center_axis',(0.,0.,1.));
#13123=DIRECTION('ref_axis',(1.,0.,0.));
#37761=CARTESIAN_POINT('',(0.,0.,0.));
#37762=CARTESIAN_POINT('Origin',(0.,0.,0.));
#37763=CARTESIAN_POINT('',(-2.94437861999191,0.00228824954296311,0.322176117089596));
#37764=CARTESIAN_POINT('',(-2.94436911647834,0.00312614869137163,0.177823882910396));
#37765=CARTESIAN_POINT('',(-2.942,-3.60291088309151E-16,0.));
#37766=CARTESIAN_POINT('',(1.28892185405323,2.64462557919717,0.));
#37767=CARTESIAN_POINT('Ctrl Pts',(-2.94437861999191,0.00228824954296311,
0.322176117089596));
#37768=CARTESIAN_POINT('Ctrl Pts',(-2.94551635113874,0.142778583613822,
0.314557432409286));
#37769=CARTESIAN_POINT('Ctrl Pts',(-2.93631267309395,0.283111895578672,
0.306938747728977));
#37770=CARTESIAN_POINT('Ctrl Pts',(-2.91624915612822,0.42186500989966,0.299320063048668));
#37771=CARTESIAN_POINT('Ctrl Pts',(-2.77830971889191,1.37581174500659,0.246940558544163));
#37772=CARTESIAN_POINT('Ctrl Pts',(-2.1270526803082,2.25506646395135,0.194561054039658));
#37773=CARTESIAN_POINT('Ctrl Pts',(-1.25475282359973,2.66583045735473,0.142181549535154));
#37774=CARTESIAN_POINT('Ctrl Pts',(-0.46548135530728,3.03749657388775,0.0947876996901026));
#37775=CARTESIAN_POINT('Ctrl Pts',(0.504756374147381,3.02561249996607,0.0473938498450515));
#37776=CARTESIAN_POINT('Ctrl Pts',(1.29197400994443,2.64783394680711,3.05745012640912E-16));
#37777=CARTESIAN_POINT('',(-1.28892185405326,2.64462557919716,0.));
#37778=CARTESIAN_POINT('Origin',(0.,0.,0.));
#37779=CARTESIAN_POINT('Ctrl Pts',(-1.28892185405326,2.64462557919716,1.87350135405495E-15));
#37780=CARTESIAN_POINT('Ctrl Pts',(-2.16038499609478,2.21989706654312,0.0524451052237091));
#37781=CARTESIAN_POINT('Ctrl Pts',(-2.79846764402885,1.33473338532309,0.104890210447416));
#37782=CARTESIAN_POINT('Ctrl Pts',(-2.92193100282573,0.379041548713593,
0.157335315671123));
#37783=CARTESIAN_POINT('Ctrl Pts',(-2.93800868581449,0.25458915624929,0.164164838084214));
#37784=CARTESIAN_POINT('Ctrl Pts',(-2.94535953294187,0.128940758021734,
0.170994360497305));
#37785=CARTESIAN_POINT('Ctrl Pts',(-2.94436911647834,0.00312614869137163,
0.177823882910396));
#37786=CARTESIAN_POINT('Origin',(0.,0.,0.));
#37787=CARTESIAN_POINT('',(-2.93740032720055,-0.000139020310086779,1.32217611708959));
#37788=CARTESIAN_POINT('',(-2.93737720095951,0.000230872487724698,1.1778238829104));
#37789=CARTESIAN_POINT('',(-2.942,-3.60291088309151E-16,0.));
#37790=CARTESIAN_POINT('Ctrl Pts',(-2.93740032720055,-0.000139020310086779,
1.32217611708959));
#37791=CARTESIAN_POINT('Ctrl Pts',(-2.93718361365059,0.494770241727901,
1.29550112610298));
#37792=CARTESIAN_POINT('Ctrl Pts',(-2.81848923912434,0.989776479202536,
1.26882613511636));
#37793=CARTESIAN_POINT('Ctrl Pts',(-2.58191143461274,1.4199490257311,1.24215114412975));
#37794=CARTESIAN_POINT('Ctrl Pts',(-2.11736289237333,2.26464377557798,1.18977163962524));
#37795=CARTESIAN_POINT('Ctrl Pts',(-1.19827972440715,2.85935294685526,1.13739213512074));
#37796=CARTESIAN_POINT('Ctrl Pts',(-0.2374000875181,2.93702585155106,1.08501263061624));
#37797=CARTESIAN_POINT('Ctrl Pts',(0.723479549370952,3.01469875624685,1.03263312611173));
#37798=CARTESIAN_POINT('Ctrl Pts',(1.72615565518287,2.57533539436116,0.980253621607226));
#37799=CARTESIAN_POINT('Ctrl Pts',(2.32033868002489,1.8162041612206,0.927874117102722));
#37800=CARTESIAN_POINT('Ctrl Pts',(2.9145217048669,1.05707292808004,0.875494612598217));
#37801=CARTESIAN_POINT('Ctrl Pts',(3.100211648739,-0.0218261763153739,0.823115108093712));
#37802=CARTESIAN_POINT('Ctrl Pts',(2.79403320730894,-0.935902477435646,
0.770735603589208));
#37803=CARTESIAN_POINT('Ctrl Pts',(2.48785476587888,-1.84997877855592,0.718356099084703));
#37804=CARTESIAN_POINT('Ctrl Pts',(1.68980793914667,-2.59923227640105,0.665976594580199));
#37805=CARTESIAN_POINT('Ctrl Pts',(0.75825229618776,-2.84733793424016,0.613597090075694));
#37806=CARTESIAN_POINT('Ctrl Pts',(-0.173303346771145,-3.09544359207927,
0.56121758557119));
#37807=CARTESIAN_POINT('Ctrl Pts',(-1.23836780595674,-2.84240140991237,
0.508838081066685));
#37808=CARTESIAN_POINT('Ctrl Pts',(-1.95858911760509,-2.20156094319437,
0.456458576562181));
#37809=CARTESIAN_POINT('Ctrl Pts',(-2.57405306040479,-1.65393177147606,
0.411697756737986));
#37810=CARTESIAN_POINT('Ctrl Pts',(-2.93769429310237,-0.823111776086056,
0.366936936913791));
#37811=CARTESIAN_POINT('Ctrl Pts',(-2.94437861999191,0.00228824954296311,
0.322176117089596));
#37812=CARTESIAN_POINT('Ctrl Pts',(-2.94436911647834,0.00312614869137163,
0.177823882910396));
#37813=CARTESIAN_POINT('Ctrl Pts',(-2.93775395051561,-0.837211781775621,
0.223439465721013));
#37814=CARTESIAN_POINT('Ctrl Pts',(-2.55902339432207,-1.68496462111194,
0.26905504853163));
#37815=CARTESIAN_POINT('Ctrl Pts',(-1.92306539600717,-2.23328718212897,
0.314670631342247));
#37816=CARTESIAN_POINT('Ctrl Pts',(-1.19189236073203,-2.86370408436305,
0.367115736565955));
#37817=CARTESIAN_POINT('Ctrl Pts',(-0.120702220522052,-3.09831789683223,
0.419560841789662));
#37818=CARTESIAN_POINT('Ctrl Pts',(0.807638005699694,-2.8335361097114,0.47200594701337));
#37819=CARTESIAN_POINT('Ctrl Pts',(1.73597823192144,-2.56875432259058,0.524451052237078));
#37820=CARTESIAN_POINT('Ctrl Pts',(2.52146854415495,-1.80457693587975,0.576896157460787));
#37821=CARTESIAN_POINT('Ctrl Pts',(2.81091642121069,-0.883954119006901,
0.629341262684494));
#37822=CARTESIAN_POINT('Ctrl Pts',(3.10036429826643,0.0366686978659464,
0.681786367908202));
#37823=CARTESIAN_POINT('Ctrl Pts',(2.89376974014439,1.11373694490081,0.734231473131909));
#37824=CARTESIAN_POINT('Ctrl Pts',(2.28393241469019,1.86192138048068,0.786676578355617));
#37825=CARTESIAN_POINT('Ctrl Pts',(1.674095089236,2.61010581606054,0.839121683579324));
#37826=CARTESIAN_POINT('Ctrl Pts',(0.661014996449636,3.02940644018541,0.891566788803033));
#37827=CARTESIAN_POINT('Ctrl Pts',(-0.299207810136722,2.93136603044105,
0.944011894026741));
#37828=CARTESIAN_POINT('Ctrl Pts',(-1.25943061672308,2.83332562069669,0.996456999250449));
#37829=CARTESIAN_POINT('Ctrl Pts',(-2.16679613710945,2.21794417708309,1.04890210447416));
#37830=CARTESIAN_POINT('Ctrl Pts',(-2.61293993368518,1.36206873790977,1.10134720969786));
#37831=CARTESIAN_POINT('Ctrl Pts',(-2.82979902340055,0.946049575313678,
1.12683943410204));
#37832=CARTESIAN_POINT('Ctrl Pts',(-2.93768601866802,0.47320929383844,1.15233165850622));
#37833=CARTESIAN_POINT('Ctrl Pts',(-2.93737720095951,0.000230872487724698,
1.1778238829104));
#37834=CARTESIAN_POINT('Origin',(0.,0.,0.));
#37835=CARTESIAN_POINT('',(-2.94487182720719,-0.00190539986535287,2.32217611708959));
#37836=CARTESIAN_POINT('',(-2.94409804542743,-0.00221960462873976,2.1778238829104));
#37837=CARTESIAN_POINT('',(-2.942,-3.60291088309151E-16,0.));
#37838=CARTESIAN_POINT('Ctrl Pts',(-2.94487182720719,-0.00190539986535287,
2.32217611708959));
#37839=CARTESIAN_POINT('Ctrl Pts',(-2.93849254859689,0.841069663508672,
2.27644481979667));
#37840=CARTESIAN_POINT('Ctrl Pts',(-2.55692453936773,1.68909389771769,2.23071352250375));
#37841=CARTESIAN_POINT('Ctrl Pts',(-1.91797659724234,2.23693579382214,2.18498222521083));
#37842=CARTESIAN_POINT('Ctrl Pts',(-1.18614132044426,2.86442044357863,2.13260272070633));
#37843=CARTESIAN_POINT('Ctrl Pts',(-0.116653199765081,3.09810042098425,
2.08022321620182));
#37844=CARTESIAN_POINT('Ctrl Pts',(0.810201861614963,2.83303510458914,2.02784371169732));
#37845=CARTESIAN_POINT('Ctrl Pts',(1.73705692299501,2.56796978819403,1.97546420719281));
#37846=CARTESIAN_POINT('Ctrl Pts',(2.52127892507592,1.80415917799819,1.92308470268831));
#37847=CARTESIAN_POINT('Ctrl Pts',(2.81068910755427,0.88461468761641,1.8707051981838));
#37848=CARTESIAN_POINT('Ctrl Pts',(3.10009929003262,-0.0349298027653776,
1.8183256936793));
#37849=CARTESIAN_POINT('Ctrl Pts',(2.89469765290841,-1.11020817333311,1.76594618917479));
#37850=CARTESIAN_POINT('Ctrl Pts',(2.28672630753671,-1.85833254788295,1.71356668467029));
#37851=CARTESIAN_POINT('Ctrl Pts',(1.67875496216501,-2.60645692243279,1.66118718016578));
#37852=CARTESIAN_POINT('Ctrl Pts',(0.668213908545816,-3.02742730096473,
1.60880767566128));
#37853=CARTESIAN_POINT('Ctrl Pts',(-0.291083395731117,-2.93219727380604,
1.55642817115678));
#37854=CARTESIAN_POINT('Ctrl Pts',(-1.25038070000804,-2.83696724664735,
1.50404866665227));
#37855=CARTESIAN_POINT('Ctrl Pts',(-2.15843425494271,-2.22553681379804,
1.45166916214777));
#37856=CARTESIAN_POINT('Ctrl Pts',(-2.60745407415374,-1.37248143316515,
1.39928965764326));
#37857=CARTESIAN_POINT('Ctrl Pts',(-2.82780430697652,-0.953856366540085,
1.37358514412537));
#37858=CARTESIAN_POINT('Ctrl Pts',(-2.93760915637607,-0.477042717206063,
1.34788063060748));
#37859=CARTESIAN_POINT('Ctrl Pts',(-2.93740032720055,-0.000139020310086779,
1.32217611708959));
#37860=CARTESIAN_POINT('Ctrl Pts',(-2.93737720095951,0.000230872487724698,
1.1778238829104));
#37861=CARTESIAN_POINT('Ctrl Pts',(-2.9370506885783,-0.499848321024544,
1.20477676372993));
#37862=CARTESIAN_POINT('Ctrl Pts',(-2.81577431600542,-1.00008193824477,
1.23172964454946));
#37863=CARTESIAN_POINT('Ctrl Pts',(-2.57446559490686,-1.43347457044749,
1.25868252536899));
#37864=CARTESIAN_POINT('Ctrl Pts',(-2.10492538678771,-2.27677300489839,
1.31112763059269));
#37865=CARTESIAN_POINT('Ctrl Pts',(-1.1809228977843,-2.86700043906715,1.3635727358164));
#37866=CARTESIAN_POINT('Ctrl Pts',(-0.218377608724914,-2.93852741234213,
1.41601784104011));
#37867=CARTESIAN_POINT('Ctrl Pts',(0.744167680334467,-3.01005438561711,
1.46846294626382));
#37868=CARTESIAN_POINT('Ctrl Pts',(1.74525576944982,-2.56288089799832,1.52090805148753));
#37869=CARTESIAN_POINT('Ctrl Pts',(2.33429173832943,-1.79826479808332,1.57335315671123));
#37870=CARTESIAN_POINT('Ctrl Pts',(2.92332770720905,-1.03364869816832,1.62579826193494));
#37871=CARTESIAN_POINT('Ctrl Pts',(3.10031155585293,0.0484100140428809,
1.67824336715865));
#37872=CARTESIAN_POINT('Ctrl Pts',(2.78557670999694,0.960852278151669,1.73068847238236));
#37873=CARTESIAN_POINT('Ctrl Pts',(2.47084186414094,1.87329454226046,1.78313357760607));
#37874=CARTESIAN_POINT('Ctrl Pts',(1.66438832378506,2.61612035826684,1.83557868282977));
#37875=CARTESIAN_POINT('Ctrl Pts',(0.729213057861966,2.85498007465664,1.88802378805348));
#37876=CARTESIAN_POINT('Ctrl Pts',(-0.205962208061124,3.09383979104644,
1.94046889327719));
#37877=CARTESIAN_POINT('Ctrl Pts',(-1.26985919955142,2.82873340781965,1.9929139985009));
#37878=CARTESIAN_POINT('Ctrl Pts',(-1.98360551176881,2.17898571169394,2.0453591037246));
#37879=CARTESIAN_POINT('Ctrl Pts',(-2.58452748049057,1.63194587688865,2.08951403011987));
#37880=CARTESIAN_POINT('Ctrl Pts',(-2.93724853244873,0.81225677381718,2.13366895651513));
#37881=CARTESIAN_POINT('Ctrl Pts',(-2.94409804542743,-0.00221960462873976,
2.1778238829104));
#37882=CARTESIAN_POINT('Origin',(0.,0.,0.));
#37883=CARTESIAN_POINT('',(-2.94188729812012,0.00254759896953657,3.32217611708959));
#37884=CARTESIAN_POINT('',(-2.94300132914192,0.00247067809074119,3.17782388291039));
#37885=CARTESIAN_POINT('',(-2.942,-3.60291088309151E-16,0.));
#37886=CARTESIAN_POINT('Ctrl Pts',(-2.94188729812012,0.00254759896953657,
3.32217611708959));
#37887=CARTESIAN_POINT('Ctrl Pts',(-2.94391723822425,0.231870355671395,
3.30976801799487));
#37888=CARTESIAN_POINT('Ctrl Pts',(-2.91930872547992,0.460762551320829,
3.29735991890015));
#37889=CARTESIAN_POINT('Ctrl Pts',(-2.86638309031571,0.682908266801983,
3.28495181980542));
#37890=CARTESIAN_POINT('Ctrl Pts',(-2.64296300603654,1.62067338423639,3.23257231530092));
#37891=CARTESIAN_POINT('Ctrl Pts',(-1.91492649555138,2.438214961245,3.18019281079642));
#37892=CARTESIAN_POINT('Ctrl Pts',(-1.00922037183541,2.76839122410029,3.12781330629191));
#37893=CARTESIAN_POINT('Ctrl Pts',(-0.103514248119433,3.09856748695557,
3.07543380178741));
#37894=CARTESIAN_POINT('Ctrl Pts',(0.979861488827348,2.94137843565753,3.0230542972829));
#37895=CARTESIAN_POINT('Ctrl Pts',(1.75438420282982,2.3674145763557,2.9706747927784));
#37896=CARTESIAN_POINT('Ctrl Pts',(2.5289069168323,1.79345071705387,2.91829528827389));
#37897=CARTESIAN_POINT('Ctrl Pts',(2.99457660789046,0.802712049748258,2.86591578376939));
#37898=CARTESIAN_POINT('Ctrl Pts',(2.94227021542597,-0.159880282562335,
2.81353627926488));
#37899=CARTESIAN_POINT('Ctrl Pts',(2.88996382296149,-1.12247261487293,2.76115677476038));
#37900=CARTESIAN_POINT('Ctrl Pts',(2.31968134697434,-2.0569186121885,2.70877727025587));
#37901=CARTESIAN_POINT('Ctrl Pts',(1.48752538566269,-2.54357700727495,2.65639776575137));
#37902=CARTESIAN_POINT('Ctrl Pts',(0.655369424351043,-3.0302354023614,2.60401826124687));
#37903=CARTESIAN_POINT('Ctrl Pts',(-0.438660022285117,-3.06910619521874,
2.55163875674236));
#37904=CARTESIAN_POINT('Ctrl Pts',(-1.30325595742871,-2.64273334365957,
2.49925925223786));
#37905=CARTESIAN_POINT('Ctrl Pts',(-2.1678518925723,-2.21636049210041,2.44687974773335));
#37906=CARTESIAN_POINT('Ctrl Pts',(-2.80301431622333,-1.32474399612474,
2.39450024322885));
#37907=CARTESIAN_POINT('Ctrl Pts',(-2.92350431159035,-0.368291087083228,
2.34212073872434));
#37908=CARTESIAN_POINT('Ctrl Pts',(-2.93879736301763,-0.246894422727957,
2.33547253151276));
#37909=CARTESIAN_POINT('Ctrl Pts',(-2.94579921760659,-0.124453265927633,
2.32882432430118));
#37910=CARTESIAN_POINT('Ctrl Pts',(-2.94487182720719,-0.00190539986535287,
2.32217611708959));
#37911=CARTESIAN_POINT('Ctrl Pts',(-2.94409804542743,-0.00221960462873976,
2.1778238829104));
#37912=CARTESIAN_POINT('Ctrl Pts',(-2.94538405566721,-0.155139230593375,
2.18611406173884));
#37913=CARTESIAN_POINT('Ctrl Pts',(-2.93447780370748,-0.307875103637501,
2.19440424056728));
#37914=CARTESIAN_POINT('Ctrl Pts',(-2.91073286453113,-0.458588216909009,
2.20269441939573));
#37915=CARTESIAN_POINT('Ctrl Pts',(-2.76051827213159,-1.41202544036162,
2.25513952461944));
#37916=CARTESIAN_POINT('Ctrl Pts',(-2.09649345438802,-2.28451087824219,
2.30758462984315));
#37917=CARTESIAN_POINT('Ctrl Pts',(-1.21754466145652,-2.68332862013697,
2.36002973506685));
#37918=CARTESIAN_POINT('Ctrl Pts',(-0.338595868525027,-3.08214636203174,
2.41247484029056));
#37919=CARTESIAN_POINT('Ctrl Pts',(0.755276899594388,-3.00729640794073,
2.46491994551426));
#37920=CARTESIAN_POINT('Ctrl Pts',(1.57170784623814,-2.49246924635079,2.51736505073797));
#37921=CARTESIAN_POINT('Ctrl Pts',(2.3881387928819,-1.97764208476085,2.56981015596168));
#37922=CARTESIAN_POINT('Ctrl Pts',(2.92712791805,-1.02283771567197,2.62225526118539));
#37923=CARTESIAN_POINT('Ctrl Pts',(2.94606932856971,-0.0578258660348382,
2.6747003664091));
#37924=CARTESIAN_POINT('Ctrl Pts',(2.96501073908941,0.907185983602299,2.72714547163281));
#37925=CARTESIAN_POINT('Ctrl Pts',(2.46390443496074,1.88240531378769,2.77959057685651));
#37926=CARTESIAN_POINT('Ctrl Pts',(1.66830473495772,2.42887370127543,2.83203568208022));
#37927=CARTESIAN_POINT('Ctrl Pts',(0.872705034954712,2.97534208876317,2.88448078730393));
#37928=CARTESIAN_POINT('Ctrl Pts',(-0.217388060922636,3.09305953355326,
2.93692589252764));
#37929=CARTESIAN_POINT('Ctrl Pts',(-1.11130990317228,2.72903986659667,2.98937099775135));
#37930=CARTESIAN_POINT('Ctrl Pts',(-2.00523174542191,2.36502019964009,3.04181610297505));
#37931=CARTESIAN_POINT('Ctrl Pts',(-2.70298233404385,1.51926342093683,3.09426120819876));
#37932=CARTESIAN_POINT('Ctrl Pts',(-2.89049530439613,0.572455370821353,
3.14670631342247));
#37933=CARTESIAN_POINT('Ctrl Pts',(-2.92758137029262,0.385196933861252,
3.15707883658511));
#37934=CARTESIAN_POINT('Ctrl Pts',(-2.94470877622731,0.1939857347123,3.16745135974775));
#37935=CARTESIAN_POINT('Ctrl Pts',(-2.94300132914192,0.00247067809074119,
3.17782388291039));
#37936=CARTESIAN_POINT('Origin',(0.,0.,0.));
#37937=CARTESIAN_POINT('',(-2.93815144027097,-0.00144838940242836,4.32217611708959));
#37938=CARTESIAN_POINT('',(-2.93758805006728,-0.000810565913221897,4.1778238829104));
#37939=CARTESIAN_POINT('',(-2.942,-3.60291088309151E-16,0.));
#37940=CARTESIAN_POINT('Ctrl Pts',(-2.93815144027097,-0.00144838940242836,
4.32217611708959));
#37941=CARTESIAN_POINT('Ctrl Pts',(-2.93549507201127,0.581944663119171,
4.29071171168856));
#37942=CARTESIAN_POINT('Ctrl Pts',(-2.76704590305946,1.16675179323199,4.25924730628754));
#37943=CARTESIAN_POINT('Ctrl Pts',(-2.44338137442995,1.64693751569171,4.22778290088651));
#37944=CARTESIAN_POINT('Ctrl Pts',(-1.90456974207211,2.44631350554451,4.175403396382));
#37945=CARTESIAN_POINT('Ctrl Pts',(-0.93560961338887,2.95575207374732,4.1230238918775));
#37946=CARTESIAN_POINT('Ctrl Pts',(0.0283581627927666,2.94647442485208,
4.07064438737299));
#37947=CARTESIAN_POINT('Ctrl Pts',(0.992325938974403,2.93719677595684,4.01826488286848));
#37948=CARTESIAN_POINT('Ctrl Pts',(1.95130136265442,2.40920290996356,3.96588537836398));
#37949=CARTESIAN_POINT('Ctrl Pts',(2.4746275187937,1.59960444002515,3.91350587385948));
#37950=CARTESIAN_POINT('Ctrl Pts',(2.99795367493297,0.790005970086747,3.86112636935497));
#37951=CARTESIAN_POINT('Ctrl Pts',(3.0856305635315,-0.301197103796779,3.80874686485047));
#37952=CARTESIAN_POINT('Ctrl Pts',(2.69828422619929,-1.18396704178881,3.75636736034596));
#37953=CARTESIAN_POINT('Ctrl Pts',(2.31093788886708,-2.06673697978085,3.70398785584146));
#37954=CARTESIAN_POINT('Ctrl Pts',(1.44856832560414,-2.7410737818814,3.65160835133695));
#37955=CARTESIAN_POINT('Ctrl Pts',(0.498448668458934,-2.90414611332682,
3.59922884683245));
#37956=CARTESIAN_POINT('Ctrl Pts',(-0.451670988686273,-3.06721844477224,
3.54684934232795));
#37957=CARTESIAN_POINT('Ctrl Pts',(-1.48954073971375,-2.71902630556253,
3.49446983782344));
#37958=CARTESIAN_POINT('Ctrl Pts',(-2.1490737861909,-2.01593590702758,3.44209033331894));
#37959=CARTESIAN_POINT('Ctrl Pts',(-2.65237107835254,-1.47939949597489,
3.40211892790916));
#37960=CARTESIAN_POINT('Ctrl Pts',(-2.93534805643284,-0.736191897535303,
3.36214752249938));
#37961=CARTESIAN_POINT('Ctrl Pts',(-2.94188729812012,0.00254759896953657,
3.32217611708959));
#37962=CARTESIAN_POINT('Ctrl Pts',(-2.94300132914192,0.00247067809074119,
3.17782388291039));
#37963=CARTESIAN_POINT('Ctrl Pts',(-2.93607565575577,-0.774344452547842,
3.21989646497146));
#37964=CARTESIAN_POINT('Ctrl Pts',(-2.61927127105561,-1.55615877069983,
3.26196904703253));
#37965=CARTESIAN_POINT('Ctrl Pts',(-2.06758380697847,-2.0994678941542,3.30404162909359));
#37966=CARTESIAN_POINT('Ctrl Pts',(-1.37988398712591,-2.77672378748653,
3.3564867343173));
#37967=CARTESIAN_POINT('Ctrl Pts',(-0.327208995338195,-3.08337625262348,
3.40893183954101));
#37968=CARTESIAN_POINT('Ctrl Pts',(0.616618861412321,-2.88139713307019,
3.46137694476472));
#37969=CARTESIAN_POINT('Ctrl Pts',(1.56044671816283,-2.67941801351691,3.51382204998842));
#37970=CARTESIAN_POINT('Ctrl Pts',(2.39542743987614,-1.9688073092734,3.56626715521213));
#37971=CARTESIAN_POINT('Ctrl Pts',(2.74572565546219,-1.06941987852551,3.61871226043584));
#37972=CARTESIAN_POINT('Ctrl Pts',(3.09602387104824,-0.170032447777603,
3.67115736565955));
#37973=CARTESIAN_POINT('Ctrl Pts',(2.96163958050702,0.918131709474696,3.72360247088326));
#37974=CARTESIAN_POINT('Ctrl Pts',(2.40306085127007,1.70527616384954,3.77604757610696));
#37975=CARTESIAN_POINT('Ctrl Pts',(1.84448212203313,2.49242061822439,3.82849268133067));
#37976=CARTESIAN_POINT('Ctrl Pts',(0.86170895410048,2.97854536972178,3.88093778655438));
#37977=CARTESIAN_POINT('Ctrl Pts',(-0.10290003671811,2.94483952623603,3.93338289177809));
#37978=CARTESIAN_POINT('Ctrl Pts',(-1.06750902753671,2.91113368275028,3.98582799700179));
#37979=CARTESIAN_POINT('Ctrl Pts',(-2.01395384124124,2.35759724428137,4.0382731022255));
#37980=CARTESIAN_POINT('Ctrl Pts',(-2.51622771244025,1.53338395412712,4.09071820744921));
#37981=CARTESIAN_POINT('Ctrl Pts',(-2.79430199366995,1.07707409733029,4.11975343260294));
#37982=CARTESIAN_POINT('Ctrl Pts',(-2.9362347477918,0.537799876108109,4.14878865775667));
#37983=CARTESIAN_POINT('Ctrl Pts',(-2.93758805006728,-0.000810565913221897,
4.1778238829104));
#37984=CARTESIAN_POINT('Origin',(0.,0.,0.));
#37985=CARTESIAN_POINT('',(-2.94644869531747,-0.000604754645607275,5.3221761170896));
#37986=CARTESIAN_POINT('',(-2.945679792052,-0.00146169071580815,5.1778238829104));
#37987=CARTESIAN_POINT('',(-2.942,-3.60291088309151E-16,0.));
#37988=CARTESIAN_POINT('Ctrl Pts',(-2.94644869531747,-0.000604754645607275,
5.3221761170896));
#37989=CARTESIAN_POINT('Ctrl Pts',(-2.94379550054715,0.929335583914262,
5.27165540538226));
#37990=CARTESIAN_POINT('Ctrl Pts',(-2.46604729438678,1.86162808593007,5.22113469367492));
#37991=CARTESIAN_POINT('Ctrl Pts',(-1.70849336410036,2.40074283220066,5.17061398196758));
#37992=CARTESIAN_POINT('Ctrl Pts',(-0.923066988207087,2.95969305927406,
5.11823447746308));
#37993=CARTESIAN_POINT('Ctrl Pts',(0.163133494924937,3.09600115191732,5.06585497295858));
#37994=CARTESIAN_POINT('Ctrl Pts',(1.06231690977038,2.74845383893534,5.01347546845407));
#37995=CARTESIAN_POINT('Ctrl Pts',(1.96150032461582,2.40090652595338,4.96109596394957));
#37996=CARTESIAN_POINT('Ctrl Pts',(2.67366667117468,1.56950380734618,4.90871645944506));
#37997=CARTESIAN_POINT('Ctrl Pts',(2.87899611438783,0.627612216959094,4.85633695494056));
#37998=CARTESIAN_POINT('Ctrl Pts',(3.08432555760098,-0.314279373428012,
4.80395745043605));
#37999=CARTESIAN_POINT('Ctrl Pts',(2.7828180974684,-1.36665983559502,4.75157794593155));
#38000=CARTESIAN_POINT('Ctrl Pts',(2.10987477706647,-2.05692589721429,4.69919844142705));
#38001=CARTESIAN_POINT('Ctrl Pts',(1.43693145666455,-2.74719195883355,4.64681893692254));
#38002=CARTESIAN_POINT('Ctrl Pts',(0.392552275993288,-3.07534361990509,
4.59443943241804));
#38003=CARTESIAN_POINT('Ctrl Pts',(-0.554252710038128,-2.89401445313919,
4.54205992791353));
#38004=CARTESIAN_POINT('Ctrl Pts',(-1.50105769606954,-2.71268528637328,
4.48968042340903));
#38005=CARTESIAN_POINT('Ctrl Pts',(-2.35028848746111,-2.02187529176995,
4.43730091890452));
#38006=CARTESIAN_POINT('Ctrl Pts',(-2.72057231514067,-1.13181358871689,
4.38492141440002));
#38007=CARTESIAN_POINT('Ctrl Pts',(-2.86842638565151,-0.776412580180032,
4.36400631529654));
#38008=CARTESIAN_POINT('Ctrl Pts',(-2.93991718809614,-0.389242894153138,
4.34309121619307));
#38009=CARTESIAN_POINT('Ctrl Pts',(-2.93815144027097,-0.00144838940242836,
4.32217611708959));
#38010=CARTESIAN_POINT('Ctrl Pts',(-2.93758805006728,-0.000810565913221897,
4.1778238829104));
#38011=CARTESIAN_POINT('Ctrl Pts',(-2.93867916073716,-0.435069497448956,
4.20123376298038));
#38012=CARTESIAN_POINT('Ctrl Pts',(-2.84838634229403,-0.86889693810433,
4.22464364305035));
#38013=CARTESIAN_POINT('Ctrl Pts',(-2.66438363654231,-1.25846258937073,
4.24805352312033));
#38014=CARTESIAN_POINT('Ctrl Pts',(-2.25216276075188,-2.13120570087471,
4.30049862834404));
#38015=CARTESIAN_POINT('Ctrl Pts',(-1.36961808047753,-2.78180178204309,
4.35294373356775));
#38016=CARTESIAN_POINT('Ctrl Pts',(-0.413994103635433,-2.91740931891088,
4.40538883879146));
#38017=CARTESIAN_POINT('Ctrl Pts',(0.541629873206673,-3.05301685577867,
4.45783394401517));
#38018=CARTESIAN_POINT('Ctrl Pts',(1.57033314661653,-2.67363584834587,4.51027904923887));
#38019=CARTESIAN_POINT('Ctrl Pts',(2.20908337968645,-1.9500304800975,4.56272415446258));
#38020=CARTESIAN_POINT('Ctrl Pts',(2.84783361275636,-1.22642511184914,4.61516925968629));
#38021=CARTESIAN_POINT('Ctrl Pts',(3.09663080548633,-0.158595382785209,
4.66761436491));
#38022=CARTESIAN_POINT('Ctrl Pts',(2.84348819889812,0.772815058373636,4.7200594701337));
#38023=CARTESIAN_POINT('Ctrl Pts',(2.5903455923099,1.70422549953248,4.77250457535741));
#38024=CARTESIAN_POINT('Ctrl Pts',(1.83526318640351,2.49921665278624,4.82494968058112));
#38025=CARTESIAN_POINT('Ctrl Pts',(0.918113109485756,2.79995295852677,4.87739478580482));
#38026=CARTESIAN_POINT('Ctrl Pts',(0.000963032567994487,3.1006892642673,
4.92983989102853));
#38027=CARTESIAN_POINT('Ctrl Pts',(-1.07825471536113,2.90717072249458,4.98228499625224));
#38028=CARTESIAN_POINT('Ctrl Pts',(-1.83377059439506,2.30650247319915,5.03473010147595));
#38029=CARTESIAN_POINT('Ctrl Pts',(-2.5208993779335,1.76020496324304,5.08242802862077));
#38030=CARTESIAN_POINT('Ctrl Pts',(-2.94027519175655,0.877129838501974,
5.13012595576559));
#38031=CARTESIAN_POINT('Ctrl Pts',(-2.945679792052,-0.00146169071580815,
5.1778238829104));
#38032=CARTESIAN_POINT('Origin',(0.,0.,0.));
#38033=CARTESIAN_POINT('',(-2.93949980478958,0.00219056232359141,6.3221761170896));
#38034=CARTESIAN_POINT('',(-2.94109090649655,0.00253660757586993,6.1778238829104));
#38035=CARTESIAN_POINT('',(-2.942,-3.60291088309151E-16,0.));
#38036=CARTESIAN_POINT('Ctrl Pts',(-2.93949980478958,0.00219056232359141,
6.3221761170896));
#38037=CARTESIAN_POINT('Ctrl Pts',(-2.94176361798241,0.320687415620876,
6.30497860358046));
#38038=CARTESIAN_POINT('Ctrl Pts',(-2.89395610782771,0.638523376129415,
6.28778109007132));
#38039=CARTESIAN_POINT('Ctrl Pts',(-2.79314214575126,0.938548174128603,
6.27058357656218));
#38040=CARTESIAN_POINT('Ctrl Pts',(-2.48608697885785,1.85235180335153,6.21820407205768));
#38041=CARTESIAN_POINT('Ctrl Pts',(-1.68730919078036,2.60092740470414,6.16582456755317));
#38042=CARTESIAN_POINT('Ctrl Pts',(-0.75552410366601,2.84810446618733,6.11344506304867));
#38043=CARTESIAN_POINT('Ctrl Pts',(0.176260983448343,3.09528152767051,6.06106555854416));
#38044=CARTESIAN_POINT('Ctrl Pts',(1.24105336959955,2.84106004928427,6.00868605403966));
#38045=CARTESIAN_POINT('Ctrl Pts',(1.96067583262663,2.19960587399116,5.95630654953515));
#38046=CARTESIAN_POINT('Ctrl Pts',(2.68029829565369,1.55815169869806,5.90392704503064));
#38047=CARTESIAN_POINT('Ctrl Pts',(3.05475083555665,0.52946482649812,5.85154754052614));
#38048=CARTESIAN_POINT('Ctrl Pts',(2.91587421520356,-0.424491793382225,
5.79916803602164));
#38049=CARTESIAN_POINT('Ctrl Pts',(2.77699759485047,-1.37844841326258,5.74678853151713));
#38050=CARTESIAN_POINT('Ctrl Pts',(2.12479181424134,-2.25767478082334,5.69440902701263));
#38051=CARTESIAN_POINT('Ctrl Pts',(1.25214960298458,-2.66732770639159,5.64202952250812));
#38052=CARTESIAN_POINT('Ctrl Pts',(0.379507391727844,-3.07698063195983,
5.58965001800362));
#38053=CARTESIAN_POINT('Ctrl Pts',(-0.713571250176501,-3.01706011553558,
5.53727051349912));
#38054=CARTESIAN_POINT('Ctrl Pts',(-1.53620630199898,-2.5144752771182,5.48489100899462));
#38055=CARTESIAN_POINT('Ctrl Pts',(-2.35884135382146,-2.01189043870081,
5.43251150449011));
#38056=CARTESIAN_POINT('Ctrl Pts',(-2.91103281556208,-1.0666412782903,5.3801319999856));
#38057=CARTESIAN_POINT('Ctrl Pts',(-2.94480241210512,-0.103220517333276,
5.3277524954811));
#38058=CARTESIAN_POINT('Ctrl Pts',(-2.94600079462919,-0.069031580495304,
5.32589370268393));
#38059=CARTESIAN_POINT('Ctrl Pts',(-2.94654631348559,-0.0348197596345374,
5.32403490988676));
#38060=CARTESIAN_POINT('Ctrl Pts',(-2.94644869531747,-0.000604754645607275,
5.3221761170896));
#38061=CARTESIAN_POINT('Ctrl Pts',(-2.945679792052,-0.00146169071580815,
5.1778238829104));
#38062=CARTESIAN_POINT('Ctrl Pts',(-2.94621768964176,-0.0889042840834332,
5.18257106098929));
#38063=CARTESIAN_POINT('Ctrl Pts',(-2.94265503660913,-0.176302465642187,
5.18731823906819));
#38064=CARTESIAN_POINT('Ctrl Pts',(-2.93484768462379,-0.263319805187537,
5.19206541714708));
#38065=CARTESIAN_POINT('Ctrl Pts',(-2.84859488567985,-1.22465587746066,
5.24451052237078));
#38066=CARTESIAN_POINT('Ctrl Pts',(-2.24427527765324,-2.13951006518879,
5.29695562759449));
#38067=CARTESIAN_POINT('Ctrl Pts',(-1.39390074925371,-2.59609494298297,
5.34940073281819));
#38068=CARTESIAN_POINT('Ctrl Pts',(-0.543526220854162,-3.05267982077716,
5.4018458380419));
#38069=CARTESIAN_POINT('Ctrl Pts',(0.552903227918311,-3.05099538863739,
5.45429094326562));
#38070=CARTESIAN_POINT('Ctrl Pts',(1.40187085321134,-2.59179983074767,5.50673604848932));
#38071=CARTESIAN_POINT('Ctrl Pts',(2.25083847850436,-2.13260427285796,5.55918115371303));
#38072=CARTESIAN_POINT('Ctrl Pts',(2.85234428031795,-1.21589758921833,5.61162625893673));
#38073=CARTESIAN_POINT('Ctrl Pts',(2.93564289965894,-0.254301037021637,
5.66407136416044));
#38074=CARTESIAN_POINT('Ctrl Pts',(3.01894151899992,0.707295515175046,5.71651646938415));
#38075=CARTESIAN_POINT('Ctrl Pts',(2.5840329558683,1.71378193592877,5.76896157460786));
#38076=CARTESIAN_POINT('Ctrl Pts',(1.82667504784324,2.31212597436553,5.82140667983157));
#38077=CARTESIAN_POINT('Ctrl Pts',(1.06931713981816,2.9104700128023,5.87385178505528));
#38078=CARTESIAN_POINT('Ctrl Pts',(-0.010490113100349,3.1006716689221,5.92629689027898));
#38079=CARTESIAN_POINT('Ctrl Pts',(-0.92671182736886,2.79711877487579,5.97874199550269));
#38080=CARTESIAN_POINT('Ctrl Pts',(-1.84293354163737,2.49356588082949,6.0311871007264));
#38081=CARTESIAN_POINT('Ctrl Pts',(-2.59556971725588,1.69625843661705,6.08363220595011));
#38082=CARTESIAN_POINT('Ctrl Pts',(-2.84584930505901,0.764074593638618,
6.13607731117382));
#38083=CARTESIAN_POINT('Ctrl Pts',(-2.91225724864025,0.516733559576513,
6.14999283508601));
#38084=CARTESIAN_POINT('Ctrl Pts',(-2.94329794130529,0.259896865352817,
6.16390835899821));
#38085=CARTESIAN_POINT('Ctrl Pts',(-2.94109090649655,0.00253660757586993,
6.1778238829104));
#38086=CARTESIAN_POINT('Origin',(0.,0.,0.));
#38087=CARTESIAN_POINT('',(-2.93998607517527,-0.0023358300504342,7.3221761170896));
#38088=CARTESIAN_POINT('',(-2.93846014819028,-0.00170708260597003,7.1778238829104));
#38089=CARTESIAN_POINT('',(-2.942,-3.60291088309151E-16,0.));
#38090=CARTESIAN_POINT('Ctrl Pts',(-2.93998607517527,-0.0023358300504342,
7.3221761170896));
#38091=CARTESIAN_POINT('Ctrl Pts',(-2.93483565594967,0.668801419715884,
7.28592229727415));
#38092=CARTESIAN_POINT('Ctrl Pts',(-2.70624449366069,1.34311250814063,7.2496684774587));
#38093=CARTESIAN_POINT('Ctrl Pts',(-2.28495024526271,1.86051554631288,7.21341465764326));
#38094=CARTESIAN_POINT('Ctrl Pts',(-1.67626448210673,2.60805925085354,7.16103515313876));
#38095=CARTESIAN_POINT('Ctrl Pts',(-0.665321452888303,3.02806588999372,
7.10865564863425));
#38096=CARTESIAN_POINT('Ctrl Pts',(0.293884302746592,2.93191878092119,7.05627614412975));
#38097=CARTESIAN_POINT('Ctrl Pts',(1.25309005838148,2.83577167184866,7.00389663962524));
#38098=CARTESIAN_POINT('Ctrl Pts',(2.16055854043283,2.22347081456344,6.95151713512074));
#38099=CARTESIAN_POINT('Ctrl Pts',(2.60876358347624,1.3699884259484,6.89913763061623));
#38100=CARTESIAN_POINT('Ctrl Pts',(3.05696862651966,0.516506037333356,6.84675812611173));
#38101=CARTESIAN_POINT('Ctrl Pts',(3.04591023055511,-0.578157882611513,
6.79437862160723));
#38102=CARTESIAN_POINT('Ctrl Pts',(2.58055450279311,-1.42241139605186,6.74199911710272));
#38103=CARTESIAN_POINT('Ctrl Pts',(2.11519877503111,-2.26666490949219,6.68961961259822));
#38104=CARTESIAN_POINT('Ctrl Pts',(1.19554571547167,-2.86050801642801,6.63724010809371));
#38105=CARTESIAN_POINT('Ctrl Pts',(0.234593342362696,-2.93725751088208,
6.5848606035892));
#38106=CARTESIAN_POINT('Ctrl Pts',(-0.726359030746288,-3.01400700533615,
6.5324810990847));
#38107=CARTESIAN_POINT('Ctrl Pts',(-1.72861071740481,-2.57366288730847,
6.4801015945802));
#38108=CARTESIAN_POINT('Ctrl Pts',(-2.32207028787941,-1.813974999748,6.4277220900757));
#38109=CARTESIAN_POINT('Ctrl Pts',(-2.72068210106971,-1.30371182195979,
6.39254009908033));
#38110=CARTESIAN_POINT('Ctrl Pts',(-2.93486858555413,-0.649377666932483,
6.35735810808496));
#38111=CARTESIAN_POINT('Ctrl Pts',(-2.93949980478958,0.00219056232359141,
6.3221761170896));
#38112=CARTESIAN_POINT('Ctrl Pts',(-2.94109090649655,0.00253660757586993,
6.1778238829104));
#38113=CARTESIAN_POINT('Ctrl Pts',(-2.9349800243151,-0.710047628629508,
6.21635346422191));
#38114=CARTESIAN_POINT('Ctrl Pts',(-2.67397994955092,-1.42664569379386,
6.25488304553342));
#38115=CARTESIAN_POINT('Ctrl Pts',(-2.20308134670334,-1.95680883878727,
6.29341262684494));
#38116=CARTESIAN_POINT('Ctrl Pts',(-1.5621108005568,-2.67844818649031,6.34585773206864));
#38117=CARTESIAN_POINT('Ctrl Pts',(-0.532246708275948,-3.05466664015197,
6.39830283729235));
#38118=CARTESIAN_POINT('Ctrl Pts',(0.42295609402977,-2.91612352177857,6.45074794251606));
#38119=CARTESIAN_POINT('Ctrl Pts',(1.3781588963355,-2.77758040340517,6.50319304773977));
#38120=CARTESIAN_POINT('Ctrl Pts',(2.25870040866608,-2.12427571299673,6.55563815296348));
#38121=CARTESIAN_POINT('Ctrl Pts',(2.66823777423309,-1.25027014357196,6.60808325818718));
#38122=CARTESIAN_POINT('Ctrl Pts',(3.07777513980009,-0.376264574147203,
6.66052836341089));
#38123=CARTESIAN_POINT('Ctrl Pts',(3.01630835860352,0.718441874293864,6.7129734686346));
#38124=CARTESIAN_POINT('Ctrl Pts',(2.51150440524776,1.54110800210975,6.76541857385831));
#38125=CARTESIAN_POINT('Ctrl Pts',(2.006700451892,2.36377412992563,6.81786367908202));
#38126=CARTESIAN_POINT('Ctrl Pts',(1.05855932637705,2.91439993711633,6.87030878430572));
#38127=CARTESIAN_POINT('Ctrl Pts',(0.0938513252260113,2.94514179293546,
6.92275388952943));
#38128=CARTESIAN_POINT('Ctrl Pts',(-0.870856675925038,2.9758836487546,6.97519899475314));
#38129=CARTESIAN_POINT('Ctrl Pts',(-1.85213155271217,2.48674155320215,7.02764409997685));
#38130=CARTESIAN_POINT('Ctrl Pts',(-2.40828908863565,1.69788454181399,7.08008920520056));
#38131=CARTESIAN_POINT('Ctrl Pts',(-2.75376700818296,1.2078566962645,7.11266743110384));
#38132=CARTESIAN_POINT('Ctrl Pts',(-2.93520341737875,0.60217681128353,7.14524565700712));
#38133=CARTESIAN_POINT('Ctrl Pts',(-2.93846014819028,-0.00170708260597003,
7.1778238829104));
#38134=CARTESIAN_POINT('Origin',(0.,0.,0.));
#38135=CARTESIAN_POINT('',(-2.94622250669394,0.000937675328142526,8.3221761170896));
#38136=CARTESIAN_POINT('',(-2.94656696235233,-0.000396508504380587,8.1778238829104));
#38137=CARTESIAN_POINT('',(-2.942,-3.60291088309151E-16,0.));
#38138=CARTESIAN_POINT('Ctrl Pts',(-2.94622250669394,0.000937675328142526,
8.3221761170896));
#38139=CARTESIAN_POINT('Ctrl Pts',(-2.94645073222768,0.0548930361868928,
8.31924549547236));
#38140=CARTESIAN_POINT('Ctrl Pts',(-2.94509413407217,0.108836699779164,
8.31631487385511));
#38141=CARTESIAN_POINT('Ctrl Pts',(-2.94211616003438,0.162690705921765,
8.31338425223786));
#38142=CARTESIAN_POINT('Ctrl Pts',(-2.88889031756852,1.12523262560549,8.26100474773336));
#38143=CARTESIAN_POINT('Ctrl Pts',(-2.31771549444688,2.05913344782865,8.20862524322884));
#38144=CARTESIAN_POINT('Ctrl Pts',(-1.48509504480843,2.54499674522788,8.15624573872434));
#38145=CARTESIAN_POINT('Ctrl Pts',(-0.652474595169965,3.03086004262711,
8.10386623421983));
#38146=CARTESIAN_POINT('Ctrl Pts',(0.44159148098532,3.06868581520241,8.05148672971533));
#38147=CARTESIAN_POINT('Ctrl Pts',(1.30577973958019,2.64148726651903,7.99910722521083));
#38148=CARTESIAN_POINT('Ctrl Pts',(2.16996799817506,2.21428871783565,7.94672772070633));
#38149=CARTESIAN_POINT('Ctrl Pts',(2.8042784392095,1.3220658478936,7.89434821620182));
#38150=CARTESIAN_POINT('Ctrl Pts',(2.92385476924452,0.36549831322338,7.84196871169732));
#38151=CARTESIAN_POINT('Ctrl Pts',(3.04343109927954,-0.591069221446826,
7.78958920719281));
#38152=CARTESIAN_POINT('Ctrl Pts',(2.64827331831513,-1.61198142084519,7.73720970268831));
#38153=CARTESIAN_POINT('Ctrl Pts',(1.9158389819387,-2.23876678477201,7.68483019818381));
#38154=CARTESIAN_POINT('Ctrl Pts',(1.18340464556226,-2.86555214869884,7.6324506936793));
#38155=CARTESIAN_POINT('Ctrl Pts',(0.113693753773775,-3.09821067715411,
7.58007118917479));
#38156=CARTESIAN_POINT('Ctrl Pts',(-0.812907669552306,-2.83226002346519,
7.52769168467029));
#38157=CARTESIAN_POINT('Ctrl Pts',(-1.73950909287838,-2.56630936977627,
7.47531218016578));
#38158=CARTESIAN_POINT('Ctrl Pts',(-2.52300104774206,-1.80174953394315,
7.42293267566128));
#38159=CARTESIAN_POINT('Ctrl Pts',(-2.81153277662714,-0.881929231056029,
7.37055317115678));
#38160=CARTESIAN_POINT('Ctrl Pts',(-2.90036087316611,-0.598751062127826,
7.35442748646772));
#38161=CARTESIAN_POINT('Ctrl Pts',(-2.94227697960606,-0.300857412821767,
7.33830180177866));
#38162=CARTESIAN_POINT('Ctrl Pts',(-2.93998607517527,-0.0023358300504342,
7.3221761170896));
#38163=CARTESIAN_POINT('Ctrl Pts',(-2.93846014819028,-0.00170708260597003,
7.1778238829104));
#38164=CARTESIAN_POINT('Ctrl Pts',(-2.94044617033292,-0.369968033311824,
7.19769076223082));
#38165=CARTESIAN_POINT('Ctrl Pts',(-2.87617048586605,-0.737561088352721,
7.21755764155125));
#38166=CARTESIAN_POINT('Ctrl Pts',(-2.7424268268773,-1.07785126568817,7.23742452087168));
#38167=CARTESIAN_POINT('Ctrl Pts',(-2.38936683413567,-1.97615813457835,
7.28986962609539));
#38168=CARTESIAN_POINT('Ctrl Pts',(-1.55220665359259,-2.68419994513487,
7.34231473131909));
#38169=CARTESIAN_POINT('Ctrl Pts',(-0.60776265660645,-2.88327813520494,
7.3947598365428));
#38170=CARTESIAN_POINT('Ctrl Pts',(0.336681340379679,-3.082356325275,7.44720494176651));
#38171=CARTESIAN_POINT('Ctrl Pts',(1.38840915380886,-2.77247089485864,7.49965004699022));
#38172=CARTESIAN_POINT('Ctrl Pts',(2.07402481044015,-2.09310519028348,7.55209515221392));
#38173=CARTESIAN_POINT('Ctrl Pts',(2.75964046707144,-1.41373948570832,7.60454025743763));
#38174=CARTESIAN_POINT('Ctrl Pts',(3.07914396690482,-0.364893506974353,
7.65698536266134));
#38175=CARTESIAN_POINT('Ctrl Pts',(2.8887227491853,0.5813339228528,7.70943046788505));
#38176=CARTESIAN_POINT('Ctrl Pts',(2.69830153146578,1.52756135267996,7.76187557310876));
#38177=CARTESIAN_POINT('Ctrl Pts',(1.99795559619334,2.37117023360031,7.81432067833246));
#38178=CARTESIAN_POINT('Ctrl Pts',(1.10291949457769,2.73244155291697,7.86676578355617));
#38179=CARTESIAN_POINT('Ctrl Pts',(0.207883392962048,3.09371287223363,7.91921088877988));
#38180=CARTESIAN_POINT('Ctrl Pts',(-0.881842874996807,2.97264662994661,
7.97165599400359));
#38181=CARTESIAN_POINT('Ctrl Pts',(-1.67575975122609,2.42373627051487,8.0241010992273));
#38182=CARTESIAN_POINT('Ctrl Pts',(-2.45144772506959,1.88742928765845,8.07534202712166));
#38183=CARTESIAN_POINT('Ctrl Pts',(-2.94475435076587,0.942699847726619,
8.12658295501603));
#38184=CARTESIAN_POINT('Ctrl Pts',(-2.94656696235233,-0.000396508504380587,
8.1778238829104));
#38185=CARTESIAN_POINT('Origin',(0.,0.,0.));
#38186=CARTESIAN_POINT('',(-2.93787859032851,0.00118007037484616,9.3221761170896));
#38187=CARTESIAN_POINT('',(-2.93938212312892,0.00216771032458683,9.1778238829104));
#38188=CARTESIAN_POINT('',(-2.942,-3.60291088309151E-16,0.));
#38189=CARTESIAN_POINT('Ctrl Pts',(-2.93787859032851,0.00118007037484616,
9.3221761170896));
#38190=CARTESIAN_POINT('Ctrl Pts',(-2.93938225399168,0.408942454113454,
9.30018918916604));
#38191=CARTESIAN_POINT('Ctrl Pts',(-2.86009946358647,0.816145924853212,
9.27820226124249));
#38192=CARTESIAN_POINT('Ctrl Pts',(-2.69715242952518,1.18654365111784,9.25621533331894));
#38193=CARTESIAN_POINT('Ctrl Pts',(-2.30896336853928,2.06894293121702,9.20383582881443));
#38194=CARTESIAN_POINT('Ctrl Pts',(-1.44594933104186,2.74245624053358,9.15145632430993));
#38195=CARTESIAN_POINT('Ctrl Pts',(-0.495674163844965,2.9046210644708,9.09907681980542));
#38196=CARTESIAN_POINT('Ctrl Pts',(0.454601003351916,3.06678588840801,9.04669731530092));
#38197=CARTESIAN_POINT('Ctrl Pts',(1.49213730024827,2.7176022269659,8.99431781079641));
#38198=CARTESIAN_POINT('Ctrl Pts',(2.15099835280526,2.01388208359571,8.94193830629191));
#38199=CARTESIAN_POINT('Ctrl Pts',(2.80985940536224,1.31016194022553,8.88955880178741));
#38200=CARTESIAN_POINT('Ctrl Pts',(3.09004521357986,0.251905314927287,8.8371792972829));
#38201=CARTESIAN_POINT('Ctrl Pts',(2.86572951288042,-0.685645923387644,
8.7847997927784));
#38202=CARTESIAN_POINT('Ctrl Pts',(2.64141381218099,-1.62319716170258,8.73242028827389));
#38203=CARTESIAN_POINT('Ctrl Pts',(1.91259660256449,-2.44004301303419,8.68004078376939));
#38204=CARTESIAN_POINT('Ctrl Pts',(1.00657547791151,-2.76935400264746,8.62766127926488));
#38205=CARTESIAN_POINT('Ctrl Pts',(0.100554353258536,-3.09866499226073,
8.57528177476038));
#38206=CARTESIAN_POINT('Ctrl Pts',(-0.982670686430926,-2.94044112015566,
8.52290227025587));
#38207=CARTESIAN_POINT('Ctrl Pts',(-1.75664477537062,-2.36573767553097,
8.47052276575137));
#38208=CARTESIAN_POINT('Ctrl Pts',(-2.48731518632227,-1.82318876070292,
8.42107388286411));
#38209=CARTESIAN_POINT('Ctrl Pts',(-2.94237161798714,-0.909460413780999,
8.37162499997686));
#38210=CARTESIAN_POINT('Ctrl Pts',(-2.94622250669394,0.000937675328142526,
8.3221761170896));
#38211=CARTESIAN_POINT('Ctrl Pts',(-2.94656696235233,-0.000396508504380587,
8.1778238829104));
#38212=CARTESIAN_POINT('Ctrl Pts',(-2.94660955927376,-0.0225595585939061,
8.17902806023974));
#38213=CARTESIAN_POINT('Ctrl Pts',(-2.94638072162746,-0.0447217067897041,
8.18023223756908));
#38214=CARTESIAN_POINT('Ctrl Pts',(-2.94587773547044,-0.0668776312364038,
8.18143641489842));
#38215=CARTESIAN_POINT('Ctrl Pts',(-2.92397135898579,-1.03182669697942,
8.23388152012213));
#38216=CARTESIAN_POINT('Ctrl Pts',(-2.3820511215168,-1.98497035188899,8.28632662534583));
#38217=CARTESIAN_POINT('Ctrl Pts',(-1.5640421648278,-2.49728659914907,8.33877173056954));
#38218=CARTESIAN_POINT('Ctrl Pts',(-0.746033208138801,-3.00960284640916,
8.39121683579325));
#38219=CARTESIAN_POINT('Ctrl Pts',(0.348064467770205,-3.08109168601973,
8.44366194101695));
#38220=CARTESIAN_POINT('Ctrl Pts',(1.22578367546087,-2.6795750856597,8.49610704624066));
#38221=CARTESIAN_POINT('Ctrl Pts',(2.10350288315153,-2.27805848529968,8.54855215146437));
#38222=CARTESIAN_POINT('Ctrl Pts',(2.76484362262384,-1.40353644496905,8.60099725668809));
#38223=CARTESIAN_POINT('Ctrl Pts',(2.91212808132915,-0.44964238612263,8.65344236191179));
#38224=CARTESIAN_POINT('Ctrl Pts',(3.05941254003446,0.504251672723784,8.7058874671355));
#38225=CARTESIAN_POINT('Ctrl Pts',(2.69264071797276,1.537517750086,8.75833257235921));
#38226=CARTESIAN_POINT('Ctrl Pts',(1.97690123029279,2.18506974304829,8.81077767758291));
#38227=CARTESIAN_POINT('Ctrl Pts',(1.26116174261282,2.83262173601059,8.86322278280662));
#38228=CARTESIAN_POINT('Ctrl Pts',(0.196454589314577,3.09445964457298,8.91566788803033));
#38229=CARTESIAN_POINT('Ctrl Pts',(-0.737982063629216,2.8527269003752,8.96811299325404));
#38230=CARTESIAN_POINT('Ctrl Pts',(-1.672418716573,2.61099415617743,9.02055809847774));
#38231=CARTESIAN_POINT('Ctrl Pts',(-2.47658486916233,1.86569075921951,9.07300320370145));
#38232=CARTESIAN_POINT('Ctrl Pts',(-2.78851523225651,0.952287217651892,
9.12544830892515));
#38233=CARTESIAN_POINT('Ctrl Pts',(-2.89235416848512,0.648223031136026,
9.1429068335869));
#38234=CARTESIAN_POINT('Ctrl Pts',(-2.94164516567622,0.325530543639097,
9.16036535824865));
#38235=CARTESIAN_POINT('Ctrl Pts',(-2.93938212312892,0.00216771032458683,
9.1778238829104));
#38236=CARTESIAN_POINT('Origin',(0.,0.,0.));
#38237=CARTESIAN_POINT('',(-2.94242444587263,-0.00248500551853048,10.3221761170896));
#38238=CARTESIAN_POINT('',(-2.93989309841074,-0.00232834448912937,10.1778238829104));
#38239=CARTESIAN_POINT('',(-2.942,-3.60291088309151E-16,0.));
#38240=CARTESIAN_POINT('Ctrl Pts',(-2.94242444587263,-0.00248500551853048,
10.3221761170896));
#38241=CARTESIAN_POINT('Ctrl Pts',(-2.93565996783783,0.755676872330999,
10.2811328828597));
#38242=CARTESIAN_POINT('Ctrl Pts',(-2.63573211439715,1.5185652175411,10.2400896486299));
#38243=CARTESIAN_POINT('Ctrl Pts',(-2.10792737213773,2.05892622612073,10.1990464144));
#38244=CARTESIAN_POINT('Ctrl Pts',(-1.43434130141424,2.74853664338077,10.1466669098955));
#38245=CARTESIAN_POINT('Ctrl Pts',(-0.389613404070186,3.07571802003838,
10.094287405391));
#38246=CARTESIAN_POINT('Ctrl Pts',(0.557026464387836,2.89349108573471,10.0419079008865));
#38247=CARTESIAN_POINT('Ctrl Pts',(1.50366633284582,2.71126415143105,9.98952839638201));
#38248=CARTESIAN_POINT('Ctrl Pts',(2.35221817241779,2.01962890616612,9.9371488918775));
#38249=CARTESIAN_POINT('Ctrl Pts',(2.72164717416933,1.12921048240304,9.884769387373));
#38250=CARTESIAN_POINT('Ctrl Pts',(3.09107617592089,0.238792058639911,9.83238988286849));
#38251=CARTESIAN_POINT('Ctrl Pts',(2.981382339852,-0.85040954362138,9.78001037836398));
#38252=CARTESIAN_POINT('Ctrl Pts',(2.44180970997212,-1.64926869616342,9.72763087385948));
#38253=CARTESIAN_POINT('Ctrl Pts',(1.90223708009224,-2.44812784870545,9.67525136935497));
#38254=CARTESIAN_POINT('Ctrl Pts',(0.93278565640137,-2.95664455152821,9.62287186485046));
#38255=CARTESIAN_POINT('Ctrl Pts',(-0.031174037472469,-2.94644704900523,
9.57049236034596));
#38256=CARTESIAN_POINT('Ctrl Pts',(-0.995133731346301,-2.93624954648225,
9.51811285584146));
#38257=CARTESIAN_POINT('Ctrl Pts',(-1.9536016954031,-2.40733783861356,9.46573335133695));
#38258=CARTESIAN_POINT('Ctrl Pts',(-2.4761536351943,-1.5972393592383,9.41335384683245));
#38259=CARTESIAN_POINT('Ctrl Pts',(-2.77935810415337,-1.1271894741653,9.3829612702515));
#38260=CARTESIAN_POINT('Ctrl Pts',(-2.93580007289335,-0.56247072784923,
9.35256869367055));
#38261=CARTESIAN_POINT('Ctrl Pts',(-2.93787859032851,0.00118007037484616,
9.3221761170896));
#38262=CARTESIAN_POINT('Ctrl Pts',(-2.93938212312892,0.00216771032458683,
9.1778238829104));
#38263=CARTESIAN_POINT('Ctrl Pts',(-2.93484702512206,-0.645845798130107,
9.21281046347236));
#38264=CARTESIAN_POINT('Ctrl Pts',(-2.72327366311651,-1.29655137950586,
9.24779704403432));
#38265=CARTESIAN_POINT('Ctrl Pts',(-2.32875660055073,-1.80542543875765,
9.28278362459629));
#38266=CARTESIAN_POINT('Ctrl Pts',(-1.73737303215174,-2.56823086742229,
9.33522872981999));
#38267=CARTESIAN_POINT('Ctrl Pts',(-0.73491132175476,-3.01233803857425,
9.3876738350437));
#38268=CARTESIAN_POINT('Ctrl Pts',(0.227407657021308,-2.93784857599215,
9.44011894026741));
#38269=CARTESIAN_POINT('Ctrl Pts',(1.1897266357974,-2.86335911341005,9.49256404549111));
#38270=CARTESIAN_POINT('Ctrl Pts',(2.11190288295256,-2.27027301709385,9.54500915071482));
#38271=CARTESIAN_POINT('Ctrl Pts',(2.57885359588429,-1.42554607687093,9.59745425593853));
#38272=CARTESIAN_POINT('Ctrl Pts',(3.045804308816,-0.580819136648041,9.64989936116224));
#38273=CARTESIAN_POINT('Ctrl Pts',(3.05752948752431,0.515548647481566,9.70234446638595));
#38274=CARTESIAN_POINT('Ctrl Pts',(2.60875076544854,1.37006875926759,9.75478957160966));
#38275=CARTESIAN_POINT('Ctrl Pts',(2.15997204337277,2.22458887105361,9.80723467683336));
#38276=CARTESIAN_POINT('Ctrl Pts',(1.25068942051291,2.83726131049606,9.85967978205706));
#38277=CARTESIAN_POINT('Ctrl Pts',(0.290183858659324,2.93231357229399,9.91212488728077));
#38278=CARTESIAN_POINT('Ctrl Pts',(-0.67032170319427,3.02736583409193,9.96456999250448));
#38279=CARTESIAN_POINT('Ctrl Pts',(-1.68205020404159,2.60479791824536,10.0170150977282));
#38280=CARTESIAN_POINT('Ctrl Pts',(-2.28961248249041,1.85481470515708,10.0694602029519));
#38281=CARTESIAN_POINT('Ctrl Pts',(-2.708067067946,1.33826862311137,10.1055814296047));
#38282=CARTESIAN_POINT('Ctrl Pts',(-2.93479827488144,0.666407318052135,
10.1417026562576));
#38283=CARTESIAN_POINT('Ctrl Pts',(-2.93989309841074,-0.00232834448912937,
10.1778238829104));
#38284=CARTESIAN_POINT('Origin',(0.,0.,-1.84858989190501));
#38285=CARTESIAN_POINT('',(-2.3720921752204,-0.00200333509135781,10.651410108095));
#38286=CARTESIAN_POINT('',(-2.37533330856671,0.000645282184899808,10.848589891905));
#38287=CARTESIAN_POINT('',(-2.37175,-1.78696459712734E-13,-1.84858989190501));
#38288=CARTESIAN_POINT('',(-2.34668236863852,0.343918483395543,11.62825));
#38289=CARTESIAN_POINT('Ctrl Pts',(-2.3720921752204,-0.00200333509135741,
10.651410108095));
#38290=CARTESIAN_POINT('Ctrl Pts',(-2.37359839777753,-0.170820576644891,
10.6627463783696));
#38291=CARTESIAN_POINT('Ctrl Pts',(-2.28072670946568,-1.11802807678178,
10.7264621531488));
#38292=CARTESIAN_POINT('Ctrl Pts',(-1.0098707589218,-2.60498459805753,10.8425574324324));
#38293=CARTESIAN_POINT('Ctrl Pts',(1.61803174729613,-2.2773674076414,10.999695945946));
#38294=CARTESIAN_POINT('Ctrl Pts',(2.79127527466209,0.0946110570183949,
11.1568344594594));
#38295=CARTESIAN_POINT('Ctrl Pts',(1.46022534703361,2.38369320998594,11.313972972973));
#38296=CARTESIAN_POINT('Ctrl Pts',(-1.1878082887304,2.52773050943662,11.4711114864865));
#38297=CARTESIAN_POINT('Ctrl Pts',(-2.23349531079268,1.11623543008163,11.5758704954955));
#38298=CARTESIAN_POINT('Ctrl Pts',(-2.34668236863853,0.343918483395475,
11.62825));
#38299=CARTESIAN_POINT('',(-0.439445221994028,2.33068358199191,11.62825));
#38300=CARTESIAN_POINT('Origin',(0.,0.,11.62825));
#38301=CARTESIAN_POINT('Ctrl Pts',(-2.37533330856671,0.000645282184899929,
10.848589891905));
#38302=CARTESIAN_POINT('Ctrl Pts',(-2.37266626526946,-0.74297942345447,
10.8986961737085));
#38303=CARTESIAN_POINT('Ctrl Pts',(-1.5987407489101,-2.26979394046941,11.0012475607357));
#38304=CARTESIAN_POINT('Ctrl Pts',(0.989622905930635,-2.61290295808564,
11.1562440529866));
#38305=CARTESIAN_POINT('Ctrl Pts',(2.72902843688469,-0.61088887604173,11.3135793686578));
#38306=CARTESIAN_POINT('Ctrl Pts',(2.00599839187704,1.9449087769569,11.4709146843289));
#38307=CARTESIAN_POINT('Ctrl Pts',(0.328567026486064,2.47549058867235,11.5758048947763));
#38308=CARTESIAN_POINT('Ctrl Pts',(-0.439445221994061,2.3306835819919,11.62825));
#38309=CARTESIAN_POINT('Origin',(0.,0.,-1.84858989190501));
#38310=CARTESIAN_POINT('',(-2.36842744616303,0.000951336475574988,9.65141010809499));
#38311=CARTESIAN_POINT('',(-2.37005148067835,-0.00187703978340947,9.84858989190503));
#38312=CARTESIAN_POINT('',(-2.37175,-1.78696459712734E-13,-1.84858989190501));
#38313=CARTESIAN_POINT('Ctrl Pts',(-2.36842744616303,0.000951336475575049,
9.65141010809499));
#38314=CARTESIAN_POINT('Ctrl Pts',(-2.36675180927421,-0.453446617531184,
9.68180268467594));
#38315=CARTESIAN_POINT('Ctrl Pts',(-2.02327622703562,-1.69331275929724,
9.76457476576139));
#38316=CARTESIAN_POINT('Ctrl Pts',(-0.0295588149451427,-2.79350652787453,
9.89972635135136));
#38317=CARTESIAN_POINT('Ctrl Pts',(2.31506703223917,-1.56365490661018,10.0568648648649));
#38318=CARTESIAN_POINT('Ctrl Pts',(2.58036243233743,1.07058768363104,10.2140033783784));
#38319=CARTESIAN_POINT('Ctrl Pts',(0.528133174514654,2.74331293137788,10.3711418918919));
#38320=CARTESIAN_POINT('Ctrl Pts',(-1.81626974066498,2.00910742659655,10.5169441351307));
#38321=CARTESIAN_POINT('Ctrl Pts',(-2.36663886088356,0.609203474490441,
10.6103668738651));
#38322=CARTESIAN_POINT('Ctrl Pts',(-2.3720921752204,-0.00200333509135741,
10.651410108095));
#38323=CARTESIAN_POINT('Ctrl Pts',(-2.37005148067835,-0.0018770397834093,
9.84858989190503));
#38324=CARTESIAN_POINT('Ctrl Pts',(-2.37190764427919,-0.245513112411714,
9.8649137704759));
#38325=CARTESIAN_POINT('Ctrl Pts',(-2.22599738542921,-1.26973141402768,
9.93368275427047));
#38326=CARTESIAN_POINT('Ctrl Pts',(-0.757654725048104,-2.69016151139635,
10.0548968432888));
#38327=CARTESIAN_POINT('Ctrl Pts',(1.83027666927001,-2.11210170665972,10.2122321589599));
#38328=CARTESIAN_POINT('Ctrl Pts',(2.77060484795253,0.367287133540841,10.369567474631));
#38329=CARTESIAN_POINT('Ctrl Pts',(1.21665350181368,2.51610800548609,10.5269027903021));
#38330=CARTESIAN_POINT('Ctrl Pts',(-1.43234772356642,2.39972494583597,10.6842381059733));
#38331=CARTESIAN_POINT('Ctrl Pts',(-2.35921176770024,0.848280000432971,
10.7914671398409));
#38332=CARTESIAN_POINT('Ctrl Pts',(-2.37545779881228,0.0353556381482985,
10.8462510684848));
#38333=CARTESIAN_POINT('Ctrl Pts',(-2.37533330856671,0.000645282184899929,
10.848589891905));
#38334=CARTESIAN_POINT('Origin',(0.,0.,-1.84858989190501));
#38335=CARTESIAN_POINT('',(-2.37515405515002,0.000755925037124906,8.65141010809499));
#38336=CARTESIAN_POINT('',(-2.36963954810708,0.00174754145538428,8.84858989190503));
#38337=CARTESIAN_POINT('',(-2.37175,-1.78696459712734E-13,-1.84858989190501));
#38338=CARTESIAN_POINT('Ctrl Pts',(-2.37515405515002,0.00075592503712492,
8.65141010809499));
#38339=CARTESIAN_POINT('Ctrl Pts',(-2.37204958700235,-0.733179040239741,
8.70085899098224));
#38340=CARTESIAN_POINT('Ctrl Pts',(-1.61660279875904,-2.25007474146859,
8.80268737837401));
#38341=CARTESIAN_POINT('Ctrl Pts',(0.954326572136137,-2.62560372673677,
8.95689527027026));
#38342=CARTESIAN_POINT('Ctrl Pts',(2.71697669134881,-0.650055649344734,
9.11403378378378));
#38343=CARTESIAN_POINT('Ctrl Pts',(2.03934512373477,1.90934627218937,9.2711722972973));
#38344=CARTESIAN_POINT('Ctrl Pts',(-0.469944521571767,2.75384968723896,
9.42831081081079));
#38345=CARTESIAN_POINT('Ctrl Pts',(-2.15345863304216,1.44000181080629,9.55505674774338));
#38346=CARTESIAN_POINT('Ctrl Pts',(-2.36963965360463,0.329676840769313,
9.62942318017144));
#38347=CARTESIAN_POINT('Ctrl Pts',(-2.36842744616303,0.000951336475575049,
9.65141010809499));
#38348=CARTESIAN_POINT('Ctrl Pts',(-2.36963954810708,0.00174754145538407,
8.84858989190503));
#38349=CARTESIAN_POINT('Ctrl Pts',(-2.36598349144566,-0.520661037292834,
8.88357647246699));
#38350=CARTESIAN_POINT('Ctrl Pts',(-1.9397431197991,-1.83158688452099,8.97100815825266));
#38351=CARTESIAN_POINT('Ctrl Pts',(0.215690902196592,-2.78647992051942,
9.11088494926201));
#38352=CARTESIAN_POINT('Ctrl Pts',(2.4459813653409,-1.35209655994371,9.26822026493315));
#38353=CARTESIAN_POINT('Ctrl Pts',(2.47433880171217,1.29947749716991,9.42555558060427));
#38354=CARTESIAN_POINT('Ctrl Pts',(0.275231669725872,2.78123058171878,9.58289089627539));
#38355=CARTESIAN_POINT('Ctrl Pts',(-1.91777323438188,1.86527979947427,9.72390233337565));
#38356=CARTESIAN_POINT('Ctrl Pts',(-2.36594419049973,0.537237102851684,
9.81246866525219));
#38357=CARTESIAN_POINT('Ctrl Pts',(-2.37005148067835,-0.0018770397834093,
9.84858989190503));
#38358=CARTESIAN_POINT('Origin',(0.,0.,-1.84858989190501));
#38359=CARTESIAN_POINT('',(-2.37012643568897,-0.00188307441280249,7.65141010809499));
#38360=CARTESIAN_POINT('',(-2.37543174471759,-0.000319652972777529,7.84858989190503));
#38361=CARTESIAN_POINT('',(-2.37175,-1.78696459712734E-13,-1.84858989190501));
#38362=CARTESIAN_POINT('Ctrl Pts',(-2.37012643568897,-0.00188307441280247,
7.65141010809499));
#38363=CARTESIAN_POINT('Ctrl Pts',(-2.37197329244753,-0.242542001652036,
7.66753579278404));
#38364=CARTESIAN_POINT('Ctrl Pts',(-2.22842022339473,-1.26275955622086,
7.7360409819776));
#38365=CARTESIAN_POINT('Ctrl Pts',(-0.770711640749916,-2.68524440462409,
7.85692567567567));
#38366=CARTESIAN_POINT('Ctrl Pts',(1.81639251383808,-2.12255793467458,8.01406418918919));
#38367=CARTESIAN_POINT('Ctrl Pts',(2.77208469636934,0.346526200869026,8.1712027027027));
#38368=CARTESIAN_POINT('Ctrl Pts',(1.23799993580832,2.50437418705365,8.32834121621622));
#38369=CARTESIAN_POINT('Ctrl Pts',(-1.40800742257503,2.4128922603655,8.48547972972973));
#38370=CARTESIAN_POINT('Ctrl Pts',(-2.35469744140074,0.865004378788607,
8.59316936035599));
#38371=CARTESIAN_POINT('Ctrl Pts',(-2.37533804356255,0.0442530790537146,
8.64847948647774));
#38372=CARTESIAN_POINT('Ctrl Pts',(-2.37515405515002,0.00075592503712492,
8.65141010809499));
#38373=CARTESIAN_POINT('Ctrl Pts',(-2.37543174471759,-0.000319652972777509,
7.84858989190503));
#38374=CARTESIAN_POINT('Ctrl Pts',(-2.37546608504675,-0.0181868229420618,
7.84979406923436));
#38375=CARTESIAN_POINT('Ctrl Pts',(-2.36724692977477,-0.814184073087101,
7.9034433517874));
#38376=CARTESIAN_POINT('Ctrl Pts',(-1.48345697628832,-2.36861723168749,
8.00953773956416));
#38377=CARTESIAN_POINT('Ctrl Pts',(1.16262680634646,-2.54151354917186,8.16687305523529));
#38378=CARTESIAN_POINT('Ctrl Pts',(2.76208455499713,-0.426475157784177,
8.3242083709064));
#38379=CARTESIAN_POINT('Ctrl Pts',(1.8750440359881,2.07248692819523,8.48154368657753));
#38380=CARTESIAN_POINT('Ctrl Pts',(-0.699958537943023,2.7057439570526,8.63887900224866));
#38381=CARTESIAN_POINT('Ctrl Pts',(-2.21235813584821,1.30404785948979,8.76122773735781));
#38382=CARTESIAN_POINT('Ctrl Pts',(-2.37146394347132,0.262432721575661,
8.83113136724327));
#38383=CARTESIAN_POINT('Ctrl Pts',(-2.36963954810708,0.00174754145538407,
8.84858989190503));
#38384=CARTESIAN_POINT('Origin',(0.,0.,-1.84858989190501));
#38385=CARTESIAN_POINT('',(-2.36973441944585,0.0017659640348839,6.65141010809499));
#38386=CARTESIAN_POINT('',(-2.36889628024144,-0.00137619754296547,6.84858989190503));
#38387=CARTESIAN_POINT('',(-2.37175,-1.78696459712734E-13,-1.84858989190501));
#38388=CARTESIAN_POINT('Ctrl Pts',(-2.36973441944585,0.00176596403488379,
6.65141010809499));
#38389=CARTESIAN_POINT('Ctrl Pts',(-2.36600087280351,-0.523508321396127,
6.68659209909035));
#38390=CARTESIAN_POINT('Ctrl Pts',(-1.93625564677593,-1.83636884117464,
6.77415359459022));
#38391=CARTESIAN_POINT('Ctrl Pts',(0.222416181733502,-2.78479173243988,
6.91409459459459));
#38392=CARTESIAN_POINT('Ctrl Pts',(2.4466042959518,-1.34857753576241,7.0712331081081));
#38393=CARTESIAN_POINT('Ctrl Pts',(2.47334911304448,1.29887571249989,7.22837162162162));
#38394=CARTESIAN_POINT('Ctrl Pts',(0.278629494786153,2.77973012269657,7.38551013513513));
#38395=CARTESIAN_POINT('Ctrl Pts',(-1.91543890246215,1.86818192765693,7.52652296395959));
#38396=CARTESIAN_POINT('Ctrl Pts',(-2.36597432596829,0.539167154048567,
7.61515628827954));
#38397=CARTESIAN_POINT('Ctrl Pts',(-2.37012643568897,-0.00188307441280247,
7.65141010809499));
#38398=CARTESIAN_POINT('Ctrl Pts',(-2.36889628024144,-0.0013761975429653,
6.84858989190503));
#38399=CARTESIAN_POINT('Ctrl Pts',(-2.37049735026751,-0.298256860301772,
6.86845677122545));
#38400=CARTESIAN_POINT('Ctrl Pts',(-2.18189218700624,-1.37689100842058,
6.94076875576958));
#38401=CARTESIAN_POINT('Ctrl Pts',(-0.57644849505612,-2.73472106868152,
7.06552584553741));
#38402=CARTESIAN_POINT('Ctrl Pts',(1.96716344393165,-1.98526073259378,7.22286116120855));
#38403=CARTESIAN_POINT('Ctrl Pts',(2.73988515609665,0.551381466653972,7.38019647687966));
#38404=CARTESIAN_POINT('Ctrl Pts',(1.04609303646807,2.5916561403346,7.53753179255079));
#38405=CARTESIAN_POINT('Ctrl Pts',(-1.56924738212969,2.3010974504224,7.69366293089257));
#38406=CARTESIAN_POINT('Ctrl Pts',(-2.3739704729535,0.759975650525201,7.79734896401065));
#38407=CARTESIAN_POINT('Ctrl Pts',(-2.37543174471759,-0.000319652972777509,
7.84858989190503));
#38408=CARTESIAN_POINT('Origin',(0.,0.,-1.84858989190501));
#38409=CARTESIAN_POINT('',(-2.37533640146812,-0.000487534612837604,5.65141010809499));
#38410=CARTESIAN_POINT('',(-2.3710171167516,0.00204493508413422,5.84858989190502));
#38411=CARTESIAN_POINT('',(-2.37175,-1.78696459712734E-13,-1.84858989190501));
#38412=CARTESIAN_POINT('Ctrl Pts',(-2.37533640146812,-0.000487534612837498,
5.65141010809499));
#38413=CARTESIAN_POINT('Ctrl Pts',(-2.3754150982357,-0.0280706202968775,
5.65326890089215));
#38414=CARTESIAN_POINT('Ctrl Pts',(-2.36258260410634,-0.832851216236821,
5.70750719819383));
#38415=CARTESIAN_POINT('Ctrl Pts',(-1.45646562934828,-2.38395507960311,
5.81412499999999));
#38416=CARTESIAN_POINT('Ctrl Pts',(1.18715361157964,-2.5288733170224,5.97126351351352));
#38417=CARTESIAN_POINT('Ctrl Pts',(2.76451839080433,-0.402457473451116,
6.12840202702702));
#38418=CARTESIAN_POINT('Ctrl Pts',(1.8589019956498,2.08542976904401,6.28554054054054));
#38419=CARTESIAN_POINT('Ctrl Pts',(-0.716306714602523,2.70026640197657,
6.44267905405405));
#38420=CARTESIAN_POINT('Ctrl Pts',(-2.21563200675447,1.29517183256302,6.5646355765722));
#38421=CARTESIAN_POINT('Ctrl Pts',(-2.37155943608083,0.258528340584143,
6.63421259458585));
#38422=CARTESIAN_POINT('Ctrl Pts',(-2.36973441944585,0.00176596403488379,
6.65141010809499));
#38423=CARTESIAN_POINT('Ctrl Pts',(-2.3710171167516,0.00204493508413416,
5.84858989190502));
#38424=CARTESIAN_POINT('Ctrl Pts',(-2.36609071130836,-0.572418580286349,
5.88711947321653));
#38425=CARTESIAN_POINT('Ctrl Pts',(-1.86927748327345,-1.93646185988882,
5.97809415975175));
#38426=CARTESIAN_POINT('Ctrl Pts',(0.401163844498212,-2.76587414046649,
6.12151395151068));
#38427=CARTESIAN_POINT('Ctrl Pts',(2.53076037597685,-1.18585163930103,6.2788492671818));
#38428=CARTESIAN_POINT('Ctrl Pts',(2.38210248511723,1.46170446446183,6.43618458285292));
#38429=CARTESIAN_POINT('Ctrl Pts',(0.0890157606711408,2.793397283841,6.59351989852405));
#38430=CARTESIAN_POINT('Ctrl Pts',(-1.98453634187054,1.75978107224967,6.73098833487474));
#38431=CARTESIAN_POINT('Ctrl Pts',(-2.36627080393209,0.485456441931073,
6.81601166600174));
#38432=CARTESIAN_POINT('Ctrl Pts',(-2.36889628024144,-0.0013761975429653,
6.84858989190503));
#38433=CARTESIAN_POINT('Origin',(0.,0.,-1.84858989190501));
#38434=CARTESIAN_POINT('',(-2.36864740940268,-0.0011676470311218,4.65141010809498));
#38435=CARTESIAN_POINT('',(-2.37471653528189,-0.00117837014130401,4.84858989190502));
#38436=CARTESIAN_POINT('',(-2.37175,-1.78696459712734E-13,-1.84858989190501));
#38437=CARTESIAN_POINT('Ctrl Pts',(-2.36864740940268,-0.00116764703112199,
4.65141010809498));
#38438=CARTESIAN_POINT('Ctrl Pts',(-2.37007090104248,-0.313795660845675,
4.67232520719846));
#38439=CARTESIAN_POINT('Ctrl Pts',(-2.16810014725707,-1.40760004764448,
4.74561981080643));
#38440=CARTESIAN_POINT('Ctrl Pts',(-0.525482821607704,-2.74379331497496,
4.87129391891892));
#38441=CARTESIAN_POINT('Ctrl Pts',(2.00035639160479,-1.95015595724574,5.02843243243243));
#38442=CARTESIAN_POINT('Ctrl Pts',(2.72955454106374,0.595034417816705,5.18557094594594));
#38443=CARTESIAN_POINT('Ctrl Pts',(1.0071746643292,2.60578839251754,5.34270945945947));
#38444=CARTESIAN_POINT('Ctrl Pts',(-1.58873507575841,2.28002578161798,5.49798918017579));
#38445=CARTESIAN_POINT('Ctrl Pts',(-2.37319747737008,0.7492017916888,5.60088939638765));
#38446=CARTESIAN_POINT('Ctrl Pts',(-2.37533640146812,-0.000487534612837498,
5.65141010809499));
#38447=CARTESIAN_POINT('Ctrl Pts',(-2.37471653528189,-0.00117837014130423,
4.84858989190502));
#38448=CARTESIAN_POINT('Ctrl Pts',(-2.37515017179056,-0.0716719020310164,
4.85333706998391));
#38449=CARTESIAN_POINT('Ctrl Pts',(-2.34054813360425,-0.920521113001663,
4.91052935328651));
#38450=CARTESIAN_POINT('Ctrl Pts',(-1.32208186928512,-2.46233460804071,
5.02016674181281));
#38451=CARTESIAN_POINT('Ctrl Pts',(1.32964132424929,-2.45826079574207,5.17750205748394));
#38452=CARTESIAN_POINT('Ctrl Pts',(2.78438780839412,-0.241198514719961,
5.33483737315506));
#38453=CARTESIAN_POINT('Ctrl Pts',(1.73255804842731,2.19299676239354,5.49217268882618));
#38454=CARTESIAN_POINT('Ctrl Pts',(-0.878964234485193,2.65300095467984,
5.64950800449731));
#38455=CARTESIAN_POINT('Ctrl Pts',(-2.25346115704322,1.19692341827648,5.76831373885692));
#38456=CARTESIAN_POINT('Ctrl Pts',(-2.37279636039799,0.20952086689332,5.83467436799283));
#38457=CARTESIAN_POINT('Ctrl Pts',(-2.3710171167516,0.00204493508413416,
5.84858989190502));
#38458=CARTESIAN_POINT('Origin',(0.,0.,-1.84858989190501));
#38459=CARTESIAN_POINT('',(-2.37165914320747,0.00205379600805495,3.65141010809498));
#38460=CARTESIAN_POINT('',(-2.36819322153198,-0.000653453332863235,3.84858989190502));
#38461=CARTESIAN_POINT('',(-2.37175,-1.78696459712734E-13,-1.84858989190501));
#38462=CARTESIAN_POINT('Ctrl Pts',(-2.37165914320747,0.0020537960080548,
3.65141010809498));
#38463=CARTESIAN_POINT('Ctrl Pts',(-2.36638740749304,-0.593495286532831,
3.69138151350476));
#38464=CARTESIAN_POINT('Ctrl Pts',(-1.83931642681201,-1.97778866762885,
3.78373242341905));
#38465=CARTESIAN_POINT('Ctrl Pts',(0.47257542983782,-2.75339906613161,3.92846283783783));
#38466=CARTESIAN_POINT('Ctrl Pts',(2.55822296043148,-1.12251023841371,4.08560135135135));
#38467=CARTESIAN_POINT('Ctrl Pts',(2.34617571991457,1.51657292659299,4.24273986486486));
#38468=CARTESIAN_POINT('Ctrl Pts',(0.0268861606557786,2.79353021925399,
4.39987837837838));
#38469=CARTESIAN_POINT('Ctrl Pts',(-2.00464048744226,1.72543877128143,4.53610179278842));
#38470=CARTESIAN_POINT('Ctrl Pts',(-2.36650592693501,0.469145905762286,
4.61994570269395));
#38471=CARTESIAN_POINT('Ctrl Pts',(-2.36864740940268,-0.00116764703112199,
4.65141010809498));
#38472=CARTESIAN_POINT('Ctrl Pts',(-2.36819322153198,-0.000653453332863235,
3.84858989190502));
#38473=CARTESIAN_POINT('Ctrl Pts',(-2.36907284142701,-0.350739660290616,
3.871999771975));
#38474=CARTESIAN_POINT('Ctrl Pts',(-2.13320735842129,-1.48399610964751,
3.94785475726868));
#38475=CARTESIAN_POINT('Ctrl Pts',(-0.392663608746353,-2.76709368867159,
4.07615484778607));
#38476=CARTESIAN_POINT('Ctrl Pts',(2.09526330020315,-1.8495577562663,4.23349016345719));
#38477=CARTESIAN_POINT('Ctrl Pts',(2.69698125586998,0.732996791565816,4.39082547912832));
#38478=CARTESIAN_POINT('Ctrl Pts',(0.870808554093777,2.65568911080063,4.54816079479944));
#38479=CARTESIAN_POINT('Ctrl Pts',(-1.66053522846232,2.20178445767042,4.70074893239168));
#38480=CARTESIAN_POINT('Ctrl Pts',(-2.37035951259304,0.707115123883991,
4.8008919647602));
#38481=CARTESIAN_POINT('Ctrl Pts',(-2.37471653528189,-0.00117837014130423,
4.84858989190502));
#38482=CARTESIAN_POINT('Origin',(0.,0.,-1.84858989190501));
#38483=CARTESIAN_POINT('',(-2.37406517885066,-0.00153607482357252,2.65141010809498));
#38484=CARTESIAN_POINT('',(-2.37255724078598,0.00199178475905649,2.84858989190502));
#38485=CARTESIAN_POINT('',(-2.37175,-1.78696459712734E-13,-1.84858989190501));
#38486=CARTESIAN_POINT('Ctrl Pts',(-2.37406517885066,-0.00153607482357281,
2.65141010809498));
#38487=CARTESIAN_POINT('Ctrl Pts',(-2.37481281249436,-0.100330398866114,
2.65805831530656));
#38488=CARTESIAN_POINT('Ctrl Pts',(-2.32469515905834,-0.976735840432517,
2.71708602702265));
#38489=CARTESIAN_POINT('Ctrl Pts',(-1.23560715428754,-2.50555554774625,
2.82849324324324));
#38490=CARTESIAN_POINT('Ctrl Pts',(1.41031161531747,-2.41154623133624,2.98563175675675));
#38491=CARTESIAN_POINT('Ctrl Pts',(2.78954424185296,-0.151581281506301,
3.14277027027027));
#38492=CARTESIAN_POINT('Ctrl Pts',(1.66331845351111,2.24452793077997,3.29990878378378));
#38493=CARTESIAN_POINT('Ctrl Pts',(-0.956834235921451,2.62469088021855,
3.45704729729729));
#38494=CARTESIAN_POINT('Ctrl Pts',(-2.26971028444252,1.15040938517441,3.57421440540103));
#38495=CARTESIAN_POINT('Ctrl Pts',(-2.37329561854466,0.186926755969883,
3.63900200900026));
#38496=CARTESIAN_POINT('Ctrl Pts',(-2.37165914320747,0.0020537960080548,
3.65141010809498));
#38497=CARTESIAN_POINT('Ctrl Pts',(-2.37255724078598,0.00199178475905658,
2.84858989190502));
#38498=CARTESIAN_POINT('Ctrl Pts',(-2.36697397570993,-0.624252704055323,
2.89066247396608));
#38499=CARTESIAN_POINT('Ctrl Pts',(-1.79321255273579,-2.04018921676783,
2.98518016125086));
#38500=CARTESIAN_POINT('Ctrl Pts',(0.584848394656438,-2.73293698550247,
3.13214295375933));
#38501=CARTESIAN_POINT('Ctrl Pts',(2.60425579784155,-1.01431944186932,3.28947826943046));
#38502=CARTESIAN_POINT('Ctrl Pts',(2.27924634057658,1.61741407950708,3.44681358510158));
#38503=CARTESIAN_POINT('Ctrl Pts',(-0.0975982492034651,2.79311059143494,
3.6041489007727));
#38504=CARTESIAN_POINT('Ctrl Pts',(-2.04600507844241,1.65356799864077,3.73807433637385));
#38505=CARTESIAN_POINT('Ctrl Pts',(-2.36710223082098,0.433557734928271,
3.81955466675129));
#38506=CARTESIAN_POINT('Ctrl Pts',(-2.36819322153198,-0.000653453332863235,
3.84858989190502));
#38507=CARTESIAN_POINT('Origin',(0.,0.,-1.84858989190501));
#38508=CARTESIAN_POINT('',(-2.36804188512505,-0.000112073902353324,1.65141010809498));
#38509=CARTESIAN_POINT('',(-2.37344137975612,-0.00178937704920473,1.84858989190502));
#38510=CARTESIAN_POINT('',(-2.37175,-1.78696459712734E-13,-1.84858989190501));
#38511=CARTESIAN_POINT('Ctrl Pts',(-2.36804188512505,-0.000112073902353224,
1.65141010809498));
#38512=CARTESIAN_POINT('Ctrl Pts',(-2.36821023678956,-0.384577180330964,
1.67711462161287));
#38513=CARTESIAN_POINT('Ctrl Pts',(-2.09930421630608,-1.55226751145704,
1.75519863963526));
#38514=CARTESIAN_POINT('Ctrl Pts',(-0.275973625536248,-2.77999224892802,
1.88566216216216));
#38515=CARTESIAN_POINT('Ctrl Pts',(2.16802781286073,-1.76187209738162,2.04280067567567));
#38516=CARTESIAN_POINT('Ctrl Pts',(2.66479327803676,0.838697048159531,2.19993918918919));
#38517=CARTESIAN_POINT('Ctrl Pts',(0.76814623510466,2.68597898024514,2.3570777027027));
#38518=CARTESIAN_POINT('Ctrl Pts',(-1.70898688612053,2.14473275169325,2.50756800900463));
#38519=CARTESIAN_POINT('Ctrl Pts',(-2.36892240045369,0.678044518839718,
2.60567881080206));
#38520=CARTESIAN_POINT('Ctrl Pts',(-2.37406517885066,-0.00153607482357281,
2.65141010809498));
#38521=CARTESIAN_POINT('Ctrl Pts',(-2.37344137975612,-0.00178937704920463,
1.84858989190502));
#38522=CARTESIAN_POINT('Ctrl Pts',(-2.37447812169567,-0.12506848067989,
1.85688007073346));
#38523=CARTESIAN_POINT('Ctrl Pts',(-2.31006431944847,-1.02714724785255,
1.91761535478561));
#38524=CARTESIAN_POINT('Ctrl Pts',(-1.15481219883121,-2.54507342378116,
2.03079574406147));
#38525=CARTESIAN_POINT('Ctrl Pts',(1.49072764255621,-2.36404822464922,2.18813105973259));
#38526=CARTESIAN_POINT('Ctrl Pts',(2.79427705549031,-0.0548463935276453,
2.34546637540372));
#38527=CARTESIAN_POINT('Ctrl Pts',(1.5823475414007,2.30372918060613,2.50280169107483));
#38528=CARTESIAN_POINT('Ctrl Pts',(-1.05405113312049,2.58842974112365,2.66013700674597));
#38529=CARTESIAN_POINT('Ctrl Pts',(-2.29031280961247,1.08993341565411,2.77539974035602));
#38530=CARTESIAN_POINT('Ctrl Pts',(-2.37393373216083,0.15638533864836,2.83821736874238));
#38531=CARTESIAN_POINT('Ctrl Pts',(-2.37255724078598,0.00199178475905658,
2.84858989190502));
#38532=CARTESIAN_POINT('Origin',(0.,0.,-1.84858989190501));
#38533=CARTESIAN_POINT('',(-2.37366757034868,0.00184471646948807,0.651410108094983));
#38534=CARTESIAN_POINT('',(-2.36802324146013,0.000186122305323028,0.848589891905023));
#38535=CARTESIAN_POINT('',(-2.37175,-1.78696459712734E-13,-1.84858989190501));
#38536=CARTESIAN_POINT('Ctrl Pts',(-2.37366757034868,0.001844716469488,
0.651410108094984));
#38537=CARTESIAN_POINT('Ctrl Pts',(-2.36827887140227,-0.663567421798888,
0.696170927919177));
#38538=CARTESIAN_POINT('Ctrl Pts',(-1.73206830317985,-2.11713322740477,
0.793311252247876));
#38539=CARTESIAN_POINT('Ctrl Pts',(0.718910407331439,-2.69944634094777,
0.942831081081078));
#38540=CARTESIAN_POINT('Ctrl Pts',(2.64899289676255,-0.887370898887054,
1.09996959459459));
#38541=CARTESIAN_POINT('Ctrl Pts',(2.19990031581894,1.72195501972256,1.25710810810811));
#38542=CARTESIAN_POINT('Ctrl Pts',(-0.225079684819506,2.78455874530281,
1.41424662162162));
#38543=CARTESIAN_POINT('Ctrl Pts',(-2.08428517335687,1.58152664346482,1.54568062161725));
#38544=CARTESIAN_POINT('Ctrl Pts',(-2.36786717732013,0.39886856587965,1.62473511710837));
#38545=CARTESIAN_POINT('Ctrl Pts',(-2.36804188512505,-0.000112073902353224,
1.65141010809498));
#38546=CARTESIAN_POINT('Ctrl Pts',(-2.36802324146013,0.000186122305323062,
0.848589891905023));
#38547=CARTESIAN_POINT('Ctrl Pts',(-2.36776001721126,-0.402962357372647,
0.87554277272455));
#38548=CARTESIAN_POINT('Ctrl Pts',(-2.0797505690667,-1.59092671500009,0.954940758767785));
#38549=CARTESIAN_POINT('Ctrl Pts',(-0.207121339063888,-2.78711087979173,
1.08678385003473));
#38550=CARTESIAN_POINT('Ctrl Pts',(2.21401803077907,-1.70561830406782,1.24411916570585));
#38551=CARTESIAN_POINT('Ctrl Pts',(2.64205485235054,0.911349150745493,1.40145448137697));
#38552=CARTESIAN_POINT('Ctrl Pts',(0.691640660298454,2.70787919402874,1.5587897970481));
#38553=CARTESIAN_POINT('Ctrl Pts',(-1.74582592441822,2.10050088985172,1.70783493389078));
#38554=CARTESIAN_POINT('Ctrl Pts',(-2.36791951286044,0.654816452515466,
1.80443496550976));
#38555=CARTESIAN_POINT('Ctrl Pts',(-2.37344137975612,-0.00178937704920463,
1.84858989190502));
#38556=CARTESIAN_POINT('Origin',(0.,0.,11.5));
#38557=CARTESIAN_POINT('',(-2.86997293948595,0.000709208322249463,11.1339652973708));
#38558=CARTESIAN_POINT('Ctrl Pts',(-0.439445221994061,2.3306835819919,11.62825));
#38559=CARTESIAN_POINT('Ctrl Pts',(-0.359483020814685,2.34931149018937,
11.6247602761445));
#38560=CARTESIAN_POINT('Ctrl Pts',(-0.27871400731898,2.36341693162049,11.6212847858384));
#38561=CARTESIAN_POINT('Ctrl Pts',(-0.197463562604575,2.37318447045242,
11.6178187998135));
#38562=CARTESIAN_POINT('Ctrl Pts',(-0.114065564321399,2.38321017787593,
11.614261203328));
#38563=CARTESIAN_POINT('Ctrl Pts',(-0.0301595928545948,2.38866567182183,
11.6107136201843));
#38564=CARTESIAN_POINT('Ctrl Pts',(0.0539178478306465,2.38969830818771,
11.6071709361129));
#38565=CARTESIAN_POINT('Ctrl Pts',(0.0934462943689916,2.39018379527021,
11.6055053668855));
#38566=CARTESIAN_POINT('Ctrl Pts',(0.133012786809523,2.38969093626847,11.6038408805234));
#38567=CARTESIAN_POINT('Ctrl Pts',(0.172582728329755,2.38823118545469,11.6021769455617));
#38568=CARTESIAN_POINT('Ctrl Pts',(0.196983674678661,2.38733102488025,11.6011508741002));
#38569=CARTESIAN_POINT('Ctrl Pts',(0.221385934120707,2.38606314465001,11.6001250123152));
#38570=CARTESIAN_POINT('Ctrl Pts',(0.24578137026875,2.38442977721171,11.5990992355836));
#38571=CARTESIAN_POINT('Ctrl Pts',(0.261730484740349,2.38336192320454,11.5984286088969));
#38572=CARTESIAN_POINT('Ctrl Pts',(0.277677591321838,2.38213767553654,11.597757980196));
#38573=CARTESIAN_POINT('Ctrl Pts',(0.293603734342933,2.38075929535175,11.5970880163414));
#38574=CARTESIAN_POINT('Ctrl Pts',(0.379341030417818,2.37333888038685,11.5934813119885));
#38575=CARTESIAN_POINT('Ctrl Pts',(0.464583014225527,2.36144918428767,11.5898891320915));
#38576=CARTESIAN_POINT('Ctrl Pts',(0.548977057540434,2.34525221307984,11.5863062427765));
#38577=CARTESIAN_POINT('Ctrl Pts',(0.63410785152571,2.32891384410355,11.5826920752337));
#38578=CARTESIAN_POINT('Ctrl Pts',(0.718376786391574,2.30819252148602,11.5790873611926));
#38579=CARTESIAN_POINT('Ctrl Pts',(0.801421129360431,2.28320149524268,11.5754867285058));
#38580=CARTESIAN_POINT('Ctrl Pts',(0.851520069054253,2.26812492443856,11.5733145410529));
#38581=CARTESIAN_POINT('Ctrl Pts',(0.901173245121242,2.25149340059607,11.5711438389925));
#38582=CARTESIAN_POINT('Ctrl Pts',(0.950298631716725,2.23332291784394,11.5689734428101));
#38583=CARTESIAN_POINT('Ctrl Pts',(0.963508179039198,2.22843697457875,11.5683898351671));
#38584=CARTESIAN_POINT('Ctrl Pts',(0.976678902975083,2.22343988211883,11.5678062771152));
#38585=CARTESIAN_POINT('Ctrl Pts',(0.989796896482515,2.2183369213822,11.5672232951128));
#38586=CARTESIAN_POINT('Ctrl Pts',(1.0715488401239,2.18653503351653,11.5635901242489));
#38587=CARTESIAN_POINT('Ctrl Pts',(1.15137916677557,2.15057972741051,11.5599737688071));
#38588=CARTESIAN_POINT('Ctrl Pts',(1.22892868995964,2.11061806082819,11.5563689172299));
#38589=CARTESIAN_POINT('Ctrl Pts',(1.30609743699769,2.07085261014462,11.5527817658451));
#38590=CARTESIAN_POINT('Ctrl Pts',(1.38100867140758,2.02711976610499,11.5492060056319));
#38591=CARTESIAN_POINT('Ctrl Pts',(1.45329568150197,1.97951483102432,11.5456364028898));
#38592=CARTESIAN_POINT('Ctrl Pts',(1.51120974849783,1.94137526215855,11.5427765500327));
#38593=CARTESIAN_POINT('Ctrl Pts',(1.56743935204678,1.90074932215926,11.5399206494764));
#38594=CARTESIAN_POINT('Ctrl Pts',(1.621783737959,1.85766460010194,11.5370660098083));
#38595=CARTESIAN_POINT('Ctrl Pts',(1.64895593091511,1.83612223907328,11.5356386899743));
#38596=CARTESIAN_POINT('Ctrl Pts',(1.67565661487015,1.81396489287275,11.5342116853624));
#38597=CARTESIAN_POINT('Ctrl Pts',(1.70185926132131,1.79119431574093,11.532784659546));
#38598=CARTESIAN_POINT('Ctrl Pts',(1.71882166156475,1.77645368090452,11.5318608680083));
#38599=CARTESIAN_POINT('Ctrl Pts',(1.73557532962421,1.76145603809249,11.5309370675846));
#38600=CARTESIAN_POINT('Ctrl Pts',(1.75211281381839,1.74620161928424,11.5300131670071));
#38601=CARTESIAN_POINT('Ctrl Pts',(1.76112158754248,1.73789179381609,11.529509873329));
#38602=CARTESIAN_POINT('Ctrl Pts',(1.77006808708219,1.72950393138366,11.5290064421071));
#38603=CARTESIAN_POINT('Ctrl Pts',(1.77894146971999,1.72104732904951,11.5285034067769));
#38604=CARTESIAN_POINT('Ctrl Pts',(1.83933200754334,1.66349331791721,11.5250798449438));
#38605=CARTESIAN_POINT('Ctrl Pts',(1.8963984276916,1.60270624192685,11.5216713230637));
#38606=CARTESIAN_POINT('Ctrl Pts',(1.95011819953022,1.53907807970147,11.5182734051049));
#38607=CARTESIAN_POINT('Ctrl Pts',(2.00542449571231,1.47357076525995,11.5147751352761));
#38608=CARTESIAN_POINT('Ctrl Pts',(2.05718398574646,1.40505149787053,11.511288104956));
#38609=CARTESIAN_POINT('Ctrl Pts',(2.10533946111886,1.3339039115796,11.5078074733588));
#38610=CARTESIAN_POINT('Ctrl Pts',(2.15154257592138,1.26564085173229,11.5044679565119));
#38611=CARTESIAN_POINT('Ctrl Pts',(2.19442802485129,1.19495736996561,11.5011343300606));
#38612=CARTESIAN_POINT('Ctrl Pts',(2.23391281993103,1.12216394079048,11.4978023184486));
#38613=CARTESIAN_POINT('Ctrl Pts',(2.25118741777841,1.09031681552637,11.4963445633684));
#38614=CARTESIAN_POINT('Ctrl Pts',(2.26781067606573,1.05806553560368,11.4948871173785));
#38615=CARTESIAN_POINT('Ctrl Pts',(2.28377353610697,1.02543493097626,11.4934296224428));
#38616=CARTESIAN_POINT('Ctrl Pts',(2.29326703470383,1.00602872191068,11.4925628149854));
#38617=CARTESIAN_POINT('Ctrl Pts',(2.30252692730832,0.986488335264957,11.4916959902159));
#38618=CARTESIAN_POINT('Ctrl Pts',(2.31155107931692,0.966818908506685,11.4908290728209));
#38619=CARTESIAN_POINT('Ctrl Pts',(2.31863529945096,0.951377840034761,11.490148517611));
#38620=CARTESIAN_POINT('Ctrl Pts',(2.32557538886546,0.935854346809815,11.4894677807698));
#38621=CARTESIAN_POINT('Ctrl Pts',(2.33236053374086,0.920273937348818,11.4887878255595));
#38622=CARTESIAN_POINT('Ctrl Pts',(2.36796902716184,0.838507826532316,11.4852194152932));
#38623=CARTESIAN_POINT('Ctrl Pts',(2.39937221583678,0.755052917299449,11.4816670269197));
#38624=CARTESIAN_POINT('Ctrl Pts',(2.42650990964853,0.670313949715511,11.4781256336386));
#38625=CARTESIAN_POINT('Ctrl Pts',(2.45395171326163,0.584625382258507,11.4745445548773));
#38626=CARTESIAN_POINT('Ctrl Pts',(2.47703230477293,0.497622920338958,11.470974719015));
#38627=CARTESIAN_POINT('Ctrl Pts',(2.49564463758615,0.409696684762178,11.4674109283565));
#38628=CARTESIAN_POINT('Ctrl Pts',(2.51256694354607,0.329754279086013,11.464170735066));
#38629=CARTESIAN_POINT('Ctrl Pts',(2.52579526118549,0.24904737731457,11.460935538995));
#38630=CARTESIAN_POINT('Ctrl Pts',(2.53521313973642,0.167858755145902,11.4577014336506));
#38631=CARTESIAN_POINT('Ctrl Pts',(2.53942638325848,0.131537684050459,11.4562546032081));
#38632=CARTESIAN_POINT('Ctrl Pts',(2.54287653840534,0.0951201284473648,
11.4548079910601));
#38633=CARTESIAN_POINT('Ctrl Pts',(2.54555076253572,0.0586312673898904,
11.4533612474409));
#38634=CARTESIAN_POINT('Ctrl Pts',(2.54678080763582,0.0418477284777441,
11.4526957983935));
#38635=CARTESIAN_POINT('Ctrl Pts',(2.54784667039524,0.0250491043820508,
11.4520303215313));
#38636=CARTESIAN_POINT('Ctrl Pts',(2.54874698931854,0.00823785327091157,
11.4513647828174));
#38637=CARTESIAN_POINT('Ctrl Pts',(2.54950258918657,-0.00587112388394168,
11.4508062241208));
#38638=CARTESIAN_POINT('Ctrl Pts',(2.55014158604825,-0.0199907301096276,
11.4502475533557));
#38639=CARTESIAN_POINT('Ctrl Pts',(2.55066270854233,-0.0341027028361791,
11.4496894146469));
#38640=CARTESIAN_POINT('Ctrl Pts',(2.55400035119776,-0.124485909584641,
11.4461146935723));
#38641=CARTESIAN_POINT('Ctrl Pts',(2.55251590030915,-0.214700787372498,
11.4425560101414));
#38642=CARTESIAN_POINT('Ctrl Pts',(2.54610973516166,-0.304360270645855,
11.4390083150826));
#38643=CARTESIAN_POINT('Ctrl Pts',(2.53992350143221,-0.390941635131681,
11.4355824166973));
#38644=CARTESIAN_POINT('Ctrl Pts',(2.52914771427487,-0.477005973362024,
11.4321667651471));
#38645=CARTESIAN_POINT('Ctrl Pts',(2.51364702202946,-0.56221151242787,11.4287568135539));
#38646=CARTESIAN_POINT('Ctrl Pts',(2.4978416408886,-0.649091891634602,11.4252798343488));
#38647=CARTESIAN_POINT('Ctrl Pts',(2.47712400969773,-0.735080204165537,
11.4218087813851));
#38648=CARTESIAN_POINT('Ctrl Pts',(2.45176245019841,-0.819915179815436,
11.4183388343531));
#38649=CARTESIAN_POINT('Ctrl Pts',(2.43759878319083,-0.867292958210081,
11.4164009734618));
#38650=CARTESIAN_POINT('Ctrl Pts',(2.42198578511571,-0.914310849766526,
11.4144634574981));
#38651=CARTESIAN_POINT('Ctrl Pts',(2.40496360252248,-0.960921226687823,
11.4125254468584));
#38652=CARTESIAN_POINT('Ctrl Pts',(2.39839032938233,-0.978920254544038,
11.4117770661373));
#38653=CARTESIAN_POINT('Ctrl Pts',(2.39160484182306,-0.996863365779891,
11.4110284061025));
#38654=CARTESIAN_POINT('Ctrl Pts',(2.38462104532031,-1.01471861919519,11.4102806421704));
#38655=CARTESIAN_POINT('Ctrl Pts',(2.35196925304181,-1.09819843212604,11.4067845734384));
#38656=CARTESIAN_POINT('Ctrl Pts',(2.31495075727319,-1.17986515814379,11.4033036769767));
#38657=CARTESIAN_POINT('Ctrl Pts',(2.27389075093231,-1.25946542646749,11.3998332297369));
#38658=CARTESIAN_POINT('Ctrl Pts',(2.23207387867294,-1.34053297976178,11.3962988111666));
#38659=CARTESIAN_POINT('Ctrl Pts',(2.18606471254661,-1.41945796930655,11.3927752305933));
#38660=CARTESIAN_POINT('Ctrl Pts',(2.13615274225743,-1.49596025824322,11.3892574989426));
#38661=CARTESIAN_POINT('Ctrl Pts',(2.08602408315185,-1.57279467573233,11.385724495342));
#38662=CARTESIAN_POINT('Ctrl Pts',(2.03195810671375,-1.64718611516111,11.3821973915595));
#38663=CARTESIAN_POINT('Ctrl Pts',(1.97420160691916,-1.71882633760539,11.3786711332592));
#38664=CARTESIAN_POINT('Ctrl Pts',(1.95240508667088,-1.74586238661548,11.377340371168));
#38665=CARTESIAN_POINT('Ctrl Pts',(1.93008253152955,-1.77250629512415,11.3760097294909));
#38666=CARTESIAN_POINT('Ctrl Pts',(1.90724574604483,-1.79874022848494,11.3746789365696));
#38667=CARTESIAN_POINT('Ctrl Pts',(1.89585779635524,-1.81182222347379,11.3740153141501));
#38668=CARTESIAN_POINT('Ctrl Pts',(1.8843419621495,-1.82480225835256,11.3733516541209));
#38669=CARTESIAN_POINT('Ctrl Pts',(1.87269964124851,-1.83767804526001,11.3726879227956));
#38670=CARTESIAN_POINT('Ctrl Pts',(1.86326625859819,-1.8481108640987,11.3721501235353));
#38671=CARTESIAN_POINT('Ctrl Pts',(1.8537496389451,-1.8584753407347,11.3716122696922));
#38672=CARTESIAN_POINT('Ctrl Pts',(1.8441608279676,-1.86875948192732,11.3710749125616));
#38673=CARTESIAN_POINT('Ctrl Pts',(1.78056218360928,-1.93696996597738,11.3675108434478));
#38674=CARTESIAN_POINT('Ctrl Pts',(1.71368420494736,-2.00176842633816,11.3639624618779));
#38675=CARTESIAN_POINT('Ctrl Pts',(1.64382533951827,-2.06287172496906,11.3604247664903));
#38676=CARTESIAN_POINT('Ctrl Pts',(1.57423141411002,-2.12374328910052,11.3569004878264));
#38677=CARTESIAN_POINT('Ctrl Pts',(1.50167852811227,-2.18094842953722,11.3533868144436));
#38678=CARTESIAN_POINT('Ctrl Pts',(1.42641996197867,-2.2341772386581,11.3498788016679));
#38679=CARTESIAN_POINT('Ctrl Pts',(1.3516762241841,-2.28704192046701,11.3463947864845));
#38680=CARTESIAN_POINT('Ctrl Pts',(1.27426307539374,-2.33598522008376,11.342916354727));
#38681=CARTESIAN_POINT('Ctrl Pts',(1.19439676647842,-2.38066281826916,11.339438662505));
#38682=CARTESIAN_POINT('Ctrl Pts',(1.15339338620205,-2.40360030684365,11.3376532145659));
#38683=CARTESIAN_POINT('Ctrl Pts',(1.11174294293827,-2.42541271468527,11.3358679615534));
#38684=CARTESIAN_POINT('Ctrl Pts',(1.06947220915485,-2.44604826098259,11.334082247983));
#38685=CARTESIAN_POINT('Ctrl Pts',(1.05124776879456,-2.45494499044852,11.3333123623541));
#38686=CARTESIAN_POINT('Ctrl Pts',(1.0329023157667,-2.46362538871231,11.3325421557385));
#38687=CARTESIAN_POINT('Ctrl Pts',(1.01446903163988,-2.47207123914098,11.3317728670993));
#38688=CARTESIAN_POINT('Ctrl Pts',(0.992379075227472,-2.48219252119531,
11.3308509720972));
#38689=CARTESIAN_POINT('Ctrl Pts',(0.970156538466361,-2.49198036655811,
11.3299301186847));
#38690=CARTESIAN_POINT('Ctrl Pts',(0.94780620569595,-2.50142961190602,11.3290102203308));
#38691=CARTESIAN_POINT('Ctrl Pts',(0.865790439448149,-2.53610413356231,
11.3256346031023));
#38692=CARTESIAN_POINT('Ctrl Pts',(0.78205610317221,-2.56622272676918,11.3222718463403));
#38693=CARTESIAN_POINT('Ctrl Pts',(0.696974578785958,-2.59191739767486,
11.318917674299));
#38694=CARTESIAN_POINT('Ctrl Pts',(0.609579162327931,-2.61831086536073,
11.3154722816062));
#38695=CARTESIAN_POINT('Ctrl Pts',(0.520761565645775,-2.64003666842693,
11.3120359469267));
#38696=CARTESIAN_POINT('Ctrl Pts',(0.430899300361841,-2.65718927641842,
11.3086040360895));
#38697=CARTESIAN_POINT('Ctrl Pts',(0.343209845834361,-2.67392714557567,
11.3052551066101));
#38698=CARTESIAN_POINT('Ctrl Pts',(0.25452479015491,-2.6863100783274,11.3019103896282));
#38699=CARTESIAN_POINT('Ctrl Pts',(0.165183352753207,-2.69438132192965,
11.2985655790638));
#38700=CARTESIAN_POINT('Ctrl Pts',(0.137834848150192,-2.69685202812409,
11.2975416917191));
#38701=CARTESIAN_POINT('Ctrl Pts',(0.110424801620538,-2.69891839950379,
11.2965177956053));
#38702=CARTESIAN_POINT('Ctrl Pts',(0.08296290180991,-2.70058085938097,11.2954937672061));
#38703=CARTESIAN_POINT('Ctrl Pts',(0.0669684788561147,-2.70154911309258,
11.2948973502268));
#38704=CARTESIAN_POINT('Ctrl Pts',(0.0509564666454086,-2.70238034652659,
11.2943008883741));
#38705=CARTESIAN_POINT('Ctrl Pts',(0.0349287839010169,-2.70307458363613,
11.2937043572455));
#38706=CARTESIAN_POINT('Ctrl Pts',(0.0206834334719444,-2.70369161924033,
11.293174162388));
#38707=CARTESIAN_POINT('Ctrl Pts',(0.00643409067270473,-2.70420004997344,
11.2926442249703));
#38708=CARTESIAN_POINT('Ctrl Pts',(-0.00781400179505987,-2.70460019597085,
11.2921146711228));
#38709=CARTESIAN_POINT('Ctrl Pts',(-0.101952151334104,-2.70724398873305,
11.2886158715889));
#38710=CARTESIAN_POINT('Ctrl Pts',(-0.196088226677417,-2.7051673117304,
11.2851318105594));
#38711=CARTESIAN_POINT('Ctrl Pts',(-0.289825667638303,-2.6984813516168,
11.2816577549713));
#38712=CARTESIAN_POINT('Ctrl Pts',(-0.384631538117472,-2.69171918420471,
11.2781441017209));
#38713=CARTESIAN_POINT('Ctrl Pts',(-0.479030586990251,-2.68024208441543,
11.2746406832979));
#38714=CARTESIAN_POINT('Ctrl Pts',(-0.57262152425153,-2.66411259564997,
11.2711426029439));
#38715=CARTESIAN_POINT('Ctrl Pts',(-0.666559717691804,-2.64792326065578,
11.2676315434484));
#38716=CARTESIAN_POINT('Ctrl Pts',(-0.759684799865766,-2.62704692522732,
11.2641258617076));
#38717=CARTESIAN_POINT('Ctrl Pts',(-0.851585181919148,-2.6014943492988,
11.2606206062542));
#38718=CARTESIAN_POINT('Ctrl Pts',(-0.886047825189167,-2.59191213332561,
11.2593061354592));
#38719=CARTESIAN_POINT('Ctrl Pts',(-0.920338108563248,-2.58167179563189,
11.2579917246108));
#38720=CARTESIAN_POINT('Ctrl Pts',(-0.95443366677234,-2.57077201863537,
11.2566771125966));
#38721=CARTESIAN_POINT('Ctrl Pts',(-0.974280480974564,-2.5644273256531,
11.255911885049));
#38722=CARTESIAN_POINT('Ctrl Pts',(-0.99406130744013,-2.55785917358927,
11.2551465893396));
#38723=CARTESIAN_POINT('Ctrl Pts',(-1.01377165408274,-2.55106714297751,
11.2543811739687));
#38724=CARTESIAN_POINT('Ctrl Pts',(-1.02736841414217,-2.54638180627496,
11.2538531685848));
#38725=CARTESIAN_POINT('Ctrl Pts',(-1.04092225787931,-2.54159315279905,
11.253325470206));
#38726=CARTESIAN_POINT('Ctrl Pts',(-1.05443025528497,-2.53670205395909,
11.252798124302));
#38727=CARTESIAN_POINT('Ctrl Pts',(-1.14463510839177,-2.50403985843604,
11.2492765690056));
#38728=CARTESIAN_POINT('Ctrl Pts',(-1.23281912858369,-2.46680540724472,
11.2457698275395));
#38729=CARTESIAN_POINT('Ctrl Pts',(-1.31858159439492,-2.42506535814129,
11.242273074989));
#38730=CARTESIAN_POINT('Ctrl Pts',(-1.40311199337542,-2.38392494816353,
11.2388265569179));
#38731=CARTESIAN_POINT('Ctrl Pts',(-1.48529083212456,-2.33840727081253,
11.2353897428216));
#38732=CARTESIAN_POINT('Ctrl Pts',(-1.56472199239298,-2.28852750879454,
11.2319580127567));
#38733=CARTESIAN_POINT('Ctrl Pts',(-1.58551758994019,-2.27546866069046,
11.2310595633688));
#38734=CARTESIAN_POINT('Ctrl Pts',(-1.60612474663732,-2.26211056997792,
11.230161462454));
#38735=CARTESIAN_POINT('Ctrl Pts',(-1.62653609083598,-2.2484529714829,11.2292636271078));
#38736=CARTESIAN_POINT('Ctrl Pts',(-1.70441968299709,-2.19633965543995,
11.225837755629));
#38737=CARTESIAN_POINT('Ctrl Pts',(-1.77945485532057,-2.13986885585993,
11.222415750716));
#38738=CARTESIAN_POINT('Ctrl Pts',(-1.85149349468849,-2.07939019092048,
11.2189930066095));
#38739=CARTESIAN_POINT('Ctrl Pts',(-1.8748645479439,-2.05976946915896,11.2178825867641));
#38740=CARTESIAN_POINT('Ctrl Pts',(-1.89791995295043,-2.03972659946025,
11.2167720891179));
#38741=CARTESIAN_POINT('Ctrl Pts',(-1.92065386067013,-2.01927267290743,
11.2156613564032));
#38742=CARTESIAN_POINT('Ctrl Pts',(-1.9316413592642,-2.00938710936888,11.2151245294621));
#38743=CARTESIAN_POINT('Ctrl Pts',(-1.94255421950186,-1.99940498570623,
11.2145876221361));
#38744=CARTESIAN_POINT('Ctrl Pts',(-1.95338011991677,-1.98933864610605,
11.2140511999421));
#38745=CARTESIAN_POINT('Ctrl Pts',(-2.02242773931489,-1.92513550744723,
11.2106298978731));
#38746=CARTESIAN_POINT('Ctrl Pts',(-2.08805585991204,-1.85740773886018,
11.2072227031525));
#38747=CARTESIAN_POINT('Ctrl Pts',(-2.15015903930769,-1.7865606665237,11.2038251982962));
#38748=CARTESIAN_POINT('Ctrl Pts',(-2.21349481278046,-1.71430745552261,
11.2003602613952));
#38749=CARTESIAN_POINT('Ctrl Pts',(-2.27316487566809,-1.63880924004706,
11.1969054028151));
#38750=CARTESIAN_POINT('Ctrl Pts',(-2.32902567586957,-1.56045035084564,
11.1934559367882));
#38751=CARTESIAN_POINT('Ctrl Pts',(-2.38527990190259,-1.48153958249049,
11.1899821762823));
#38752=CARTESIAN_POINT('Ctrl Pts',(-2.43767154642151,-1.39972691196139,
11.1865138845562));
#38753=CARTESIAN_POINT('Ctrl Pts',(-2.48601414345046,-1.31537014370798,
11.1830462761383));
#38754=CARTESIAN_POINT('Ctrl Pts',(-2.51324863986033,-1.26784654664574,
11.1810927491288));
#38755=CARTESIAN_POINT('Ctrl Pts',(-2.53919729042327,-1.21951494628862,
11.1791394389872));
#38756=CARTESIAN_POINT('Ctrl Pts',(-2.56382026308967,-1.17043597842562,
11.1771854900701));
#38757=CARTESIAN_POINT('Ctrl Pts',(-2.57043915220293,-1.15724308533024,
11.1766602500274));
#38758=CARTESIAN_POINT('Ctrl Pts',(-2.57696321367054,-1.1439941193146,11.1761348825453));
#38759=CARTESIAN_POINT('Ctrl Pts',(-2.58338840616944,-1.13069688731366,
11.175609633533));
#38760=CARTESIAN_POINT('Ctrl Pts',(-2.62620034331217,-1.04209561027884,
11.172109827464));
#38761=CARTESIAN_POINT('Ctrl Pts',(-2.66450788394824,-0.951602474453648,
11.1686250464566));
#38762=CARTESIAN_POINT('Ctrl Pts',(-2.69817002472794,-0.859613847080416,
11.1651505728457));
#38763=CARTESIAN_POINT('Ctrl Pts',(-2.73183382450822,-0.767620686151626,
11.1616759279993));
#38764=CARTESIAN_POINT('Ctrl Pts',(-2.76085223666098,-0.67413102162785,
11.1582115915653));
#38765=CARTESIAN_POINT('Ctrl Pts',(-2.78504109696179,-0.579512179774996,
11.1547528451809));
#38766=CARTESIAN_POINT('Ctrl Pts',(-2.80867562760501,-0.487061692675289,
11.1513733619645));
#38767=CARTESIAN_POINT('Ctrl Pts',(-2.8276996967141,-0.393532337548253,
11.1479992155222));
#38768=CARTESIAN_POINT('Ctrl Pts',(-2.84189514122644,-0.299251761426908,
11.1446260045022));
#38769=CARTESIAN_POINT('Ctrl Pts',(-2.85324010443846,-0.223902964369238,
11.1419301428196));
#38770=CARTESIAN_POINT('Ctrl Pts',(-2.86150015598816,-0.148073915036915,
11.1392348786069));
#38771=CARTESIAN_POINT('Ctrl Pts',(-2.86653995619031,-0.0719300717664526,
11.1365379651471));
#38772=CARTESIAN_POINT('Ctrl Pts',(-2.86814414143213,-0.0476932320643782,
11.1356795285827));
#38773=CARTESIAN_POINT('Ctrl Pts',(-2.86941988081495,-0.0234547494955555,
11.1348219958471));
#38774=CARTESIAN_POINT('Ctrl Pts',(-2.87036479087719,0.000779773978368722,
11.1339652973708));
#38775=CARTESIAN_POINT('',(0.261199069988913,2.92594434598213,11.058));
#38776=CARTESIAN_POINT('Ctrl Pts',(0.261124777554784,2.92529416030266,11.058));
#38777=CARTESIAN_POINT('Ctrl Pts',(0.163252076286772,2.9214051496811,11.0703793245688));
#38778=CARTESIAN_POINT('Ctrl Pts',(0.0658388360676064,2.91286361031638,
11.0828028087884));
#38779=CARTESIAN_POINT('Ctrl Pts',(-0.0307369711720644,2.89968653111402,
11.0952900032599));
#38780=CARTESIAN_POINT('Ctrl Pts',(-0.12623809978967,2.88665608413482,11.1076382424244));
#38781=CARTESIAN_POINT('Ctrl Pts',(-0.220921197195477,2.86909236615812,
11.1200487818169));
#38782=CARTESIAN_POINT('Ctrl Pts',(-0.31439997383375,2.84696555496448,11.1325405266072));
#38783=CARTESIAN_POINT('Ctrl Pts',(-0.389995520831668,2.82907177783499,
11.1426425017756));
#38784=CARTESIAN_POINT('Ctrl Pts',(-0.464803253647579,2.80819289824412,
11.152797583885));
#38785=CARTESIAN_POINT('Ctrl Pts',(-0.538603048202427,2.78429272567688,
11.1630157713274));
#38786=CARTESIAN_POINT('Ctrl Pts',(-0.593952894118562,2.76636759625145,
11.1706794119091));
#38787=CARTESIAN_POINT('Ctrl Pts',(-0.648735503576454,2.7467426089957,11.1783785492407));
#38788=CARTESIAN_POINT('Ctrl Pts',(-0.702851172581185,2.72539620337798,
11.1861174013937));
#38789=CARTESIAN_POINT('Ctrl Pts',(-0.71873840261759,2.71912934457837,11.1883893667345));
#38790=CARTESIAN_POINT('Ctrl Pts',(-0.734568107078247,2.71271408483162,
11.190664755044));
#38791=CARTESIAN_POINT('Ctrl Pts',(-0.750337652372167,2.70614979460715,
11.1929436730527));
#38792=CARTESIAN_POINT('Ctrl Pts',(-0.763539656096334,2.70065427889159,
11.1948515456945));
#38793=CARTESIAN_POINT('Ctrl Pts',(-0.776691326847496,2.69505769580723,
11.1967607130315));
#38794=CARTESIAN_POINT('Ctrl Pts',(-0.789788993683481,2.68936106997679,
11.1986708957826));
#38795=CARTESIAN_POINT('Ctrl Pts',(-0.87317349082548,2.65309428397392,11.2108318119326));
#38796=CARTESIAN_POINT('Ctrl Pts',(-0.954403883416443,2.61276259333994,
11.2230385405707));
#38797=CARTESIAN_POINT('Ctrl Pts',(-1.03314628688233,2.56834468618871,11.2353100289649));
#38798=CARTESIAN_POINT('Ctrl Pts',(-1.07823214235908,2.54291214597843,11.2423363645588));
#38799=CARTESIAN_POINT('Ctrl Pts',(-1.12250179725942,2.51613922516579,11.2493839310575));
#38800=CARTESIAN_POINT('Ctrl Pts',(-1.16588734321926,2.48801620495338,11.2564562851141));
#38801=CARTESIAN_POINT('Ctrl Pts',(-1.2435976078222,2.43764349916415,11.2691239718505));
#38802=CARTESIAN_POINT('Ctrl Pts',(-1.31847408700313,2.38294042952196,11.2818711829841));
#38803=CARTESIAN_POINT('Ctrl Pts',(-1.39030087935118,2.32423346489716,11.2947183566611));
#38804=CARTESIAN_POINT('Ctrl Pts',(-1.46342993694969,2.26446210581046,11.3077984577361));
#38805=CARTESIAN_POINT('Ctrl Pts',(-1.53339828473794,2.20053932645019,11.3209821789827));
#38806=CARTESIAN_POINT('Ctrl Pts',(-1.59992558939365,2.1327921427514,11.3342910904939));
#38807=CARTESIAN_POINT('Ctrl Pts',(-1.61340208445737,2.11906853570881,11.3369870884937));
#38808=CARTESIAN_POINT('Ctrl Pts',(-1.62674073455187,2.10518403555254,11.3396889690338));
#38809=CARTESIAN_POINT('Ctrl Pts',(-1.63991787601809,2.09116421105248,11.3423925384684));
#38810=CARTESIAN_POINT('Ctrl Pts',(-1.70139884650346,2.02575150993609,11.3550066606613));
#38811=CARTESIAN_POINT('Ctrl Pts',(-1.75944768512028,1.95731714657644,11.3676731670409));
#38812=CARTESIAN_POINT('Ctrl Pts',(-1.8138993651727,1.88618389956551,11.3804137020214));
#38813=CARTESIAN_POINT('Ctrl Pts',(-1.86815753562372,1.81530344486993,11.393108959871));
#38814=CARTESIAN_POINT('Ctrl Pts',(-1.91884436205444,1.74174225535381,11.4058777210929));
#38815=CARTESIAN_POINT('Ctrl Pts',(-1.96574838356875,1.66580180077525,11.4187414001618));
#38816=CARTESIAN_POINT('Ctrl Pts',(-2.01186212788083,1.59114085290088,11.4313883414761));
#38817=CARTESIAN_POINT('Ctrl Pts',(-2.05431959945996,1.51417923664983,11.4441270290762));
#38818=CARTESIAN_POINT('Ctrl Pts',(-2.09287020326133,1.43520021222363,11.4569778131465));
#38819=CARTESIAN_POINT('Ctrl Pts',(-2.11361694660402,1.39269614256837,11.4638937079073));
#38820=CARTESIAN_POINT('Ctrl Pts',(-2.13323129045024,1.34960780406157,11.4708420687169));
#38821=CARTESIAN_POINT('Ctrl Pts',(-2.15166787184208,1.30598030868302,11.4778260675126));
#38822=CARTESIAN_POINT('Ctrl Pts',(-2.15713184571921,1.29305060712901,11.4798958865407));
#38823=CARTESIAN_POINT('Ctrl Pts',(-2.16249308944786,1.28007170317631,11.4819691313049));
#38824=CARTESIAN_POINT('Ctrl Pts',(-2.16774797314523,1.26705068510794,11.4840449452013));
#38825=CARTESIAN_POINT('Ctrl Pts',(-2.19963752356477,1.18803192158837,11.4966421358759));
#38826=CARTESIAN_POINT('Ctrl Pts',(-2.22751419897903,1.10771397257159,11.5092939385505));
#38827=CARTESIAN_POINT('Ctrl Pts',(-2.25120331746379,1.02636717479289,11.5220225137828));
#38828=CARTESIAN_POINT('Ctrl Pts',(-2.27454503464211,0.946213329121761,
11.5345644242532));
#38829=CARTESIAN_POINT('Ctrl Pts',(-2.29382118362004,0.865059764231561,
11.5471808720505));
#38830=CARTESIAN_POINT('Ctrl Pts',(-2.30881496364231,0.783166675687281,
11.5598930570057));
#38831=CARTESIAN_POINT('Ctrl Pts',(-2.3233692591387,0.703673965509062,11.572232633548));
#38832=CARTESIAN_POINT('Ctrl Pts',(-2.33388845327117,0.623483808186223,
11.5846624171728));
#38833=CARTESIAN_POINT('Ctrl Pts',(-2.34012749274977,0.542846284442329,
11.5972017976454));
#38834=CARTESIAN_POINT('Ctrl Pts',(-2.34523853245788,0.476787785015864,
11.6074740954455));
#38835=CARTESIAN_POINT('Ctrl Pts',(-2.34747636127652,0.410429125649976,
11.6178199429796));
#38836=CARTESIAN_POINT('Ctrl Pts',(-2.34668236863853,0.343918483395475,
11.62825));
#38837=CARTESIAN_POINT('',(-2.14415473270599,2.01243073062329,11.058));
#38838=CARTESIAN_POINT('Origin',(0.,0.,11.058));
#38839=CARTESIAN_POINT('Ctrl Pts',(-2.87036479087719,0.000779773978368722,
11.1339652973708));
#38840=CARTESIAN_POINT('Ctrl Pts',(-2.87200285191233,0.0427918449624727,
11.1324801566689));
#38841=CARTESIAN_POINT('Ctrl Pts',(-2.87264678506693,0.0847919926152422,
11.1309975229776));
#38842=CARTESIAN_POINT('Ctrl Pts',(-2.87228289058568,0.126751532711213,
11.1295170338848));
#38843=CARTESIAN_POINT('Ctrl Pts',(-2.87145802595519,0.221864106052536,
11.1261611075067));
#38844=CARTESIAN_POINT('Ctrl Pts',(-2.86545855469524,0.316767622116373,
11.1228162005919));
#38845=CARTESIAN_POINT('Ctrl Pts',(-2.85455763680452,0.411156736693552,
11.1194780920563));
#38846=CARTESIAN_POINT('Ctrl Pts',(-2.84342076253498,0.507588955704657,
11.1160677283208));
#38847=CARTESIAN_POINT('Ctrl Pts',(-2.82716775830471,0.603485022278454,
11.1126644604589));
#38848=CARTESIAN_POINT('Ctrl Pts',(-2.80603441756026,0.698520670355508,
11.1092637873076));
#38849=CARTESIAN_POINT('Ctrl Pts',(-2.79266006313991,0.75866451866233,11.1071116520374));
#38850=CARTESIAN_POINT('Ctrl Pts',(-2.77733000149192,0.818463754777881,
11.1049605559651));
#38851=CARTESIAN_POINT('Ctrl Pts',(-2.76009348614301,0.877834296726592,
11.1028093582138));
#38852=CARTESIAN_POINT('Ctrl Pts',(-2.74919109087412,0.915387195473845,
11.1014486882808));
#38853=CARTESIAN_POINT('Ctrl Pts',(-2.73752580613221,0.952768545576029,
11.1000879776682));
#38854=CARTESIAN_POINT('Ctrl Pts',(-2.72510854264357,0.989956497598032,
11.0987269376699));
#38855=CARTESIAN_POINT('Ctrl Pts',(-2.72027063675402,1.00444534308902,11.0981966611375));
#38856=CARTESIAN_POINT('Ctrl Pts',(-2.71531799003855,1.0189064745382,11.0976662739811));
#38857=CARTESIAN_POINT('Ctrl Pts',(-2.71025302608607,1.03333338889234,11.0971359498549));
#38858=CARTESIAN_POINT('Ctrl Pts',(-2.67741979989202,1.12685471435798,11.0936981658637));
#38859=CARTESIAN_POINT('Ctrl Pts',(-2.63998428261572,1.2186200392303,11.0902747408666));
#38860=CARTESIAN_POINT('Ctrl Pts',(-2.59822193704792,1.30830487286322,11.0868612068006));
#38861=CARTESIAN_POINT('Ctrl Pts',(-2.55598691495593,1.39900478155616,11.0834090375144));
#38862=CARTESIAN_POINT('Ctrl Pts',(-2.50932621498891,1.48757769234242,11.0799669843223));
#38863=CARTESIAN_POINT('Ctrl Pts',(-2.45847158858181,1.57367848927911,11.0765304257261));
#38864=CARTESIAN_POINT('Ctrl Pts',(-2.40788866695146,1.65931926911486,11.0731122278858));
#38865=CARTESIAN_POINT('Ctrl Pts',(-2.35315604081231,1.74251510638125,11.0696994660854));
#38866=CARTESIAN_POINT('Ctrl Pts',(-2.29445585803367,1.82290449738493,11.0662875925062));
#38867=CARTESIAN_POINT('Ctrl Pts',(-2.24693123162509,1.88798906090443,11.0635252839489));
#38868=CARTESIAN_POINT('Ctrl Pts',(-2.19680500482205,1.95123384018432,11.0607635576017));
#38869=CARTESIAN_POINT('Ctrl Pts',(-2.14415473270599,2.01243073062329,11.058));
#38870=CARTESIAN_POINT('',(-2.,-2.4492935982947E-16,12.));
#38871=CARTESIAN_POINT('',(-2.5,-3.06161699786838E-16,11.5));
#38872=CARTESIAN_POINT('Origin',(0.,0.,12.));
#38873=CARTESIAN_POINT('Ctrl Pts',(1.70810875200395,-2.39535560853238,-0.329233991005387));
#38874=CARTESIAN_POINT('Ctrl Pts',(2.49644455514999,-1.833199709811,-0.276854486500882));
#38875=CARTESIAN_POINT('Ctrl Pts',(3.46233357982621,0.120022568706166,-0.172095477491873));
#38876=CARTESIAN_POINT('Ctrl Pts',(1.80423238277522,2.96114098648209,-0.0149569639783592));
#38877=CARTESIAN_POINT('Ctrl Pts',(-1.47579564172449,3.13432118289611,0.142181549535154));
#38878=CARTESIAN_POINT('Ctrl Pts',(-3.42956675747562,0.496557026061836,
0.299320063048668));
#38879=CARTESIAN_POINT('Ctrl Pts',(-2.30343226514234,-2.58935922774548,
0.456458576562181));
#38880=CARTESIAN_POINT('Ctrl Pts',(0.891761112414455,-3.34848577424617,
0.613597090075694));
#38881=CARTESIAN_POINT('Ctrl Pts',(3.2859015926111,-1.1007252807108,0.770735603589207));
#38882=CARTESIAN_POINT('Ctrl Pts',(2.7288317609948,2.13597203247546,0.927874117102722));
#38883=CARTESIAN_POINT('Ctrl Pts',(-0.27919655644097,3.45406211813255,1.08501263061624));
#38884=CARTESIAN_POINT('Ctrl Pts',(-3.03644606033952,1.66993460430069,1.24215114412975));
#38885=CARTESIAN_POINT('Ctrl Pts',(-3.06648780987738,-1.61410638094873,
1.39928965764326));
#38886=CARTESIAN_POINT('Ctrl Pts',(-0.342327145073366,-3.44839767949667,
1.55642817115678));
#38887=CARTESIAN_POINT('Ctrl Pts',(2.68929601578421,-2.18548654390084,1.71356668467029));
#38888=CARTESIAN_POINT('Ctrl Pts',(3.30550092715682,1.04034856780235,1.8707051981838));
#38889=CARTESIAN_POINT('Ctrl Pts',(0.952834920914103,3.33178039838987,2.02784371169731));
#38890=CARTESIAN_POINT('Ctrl Pts',(-2.25562944112346,2.630740466173,2.18498222521083));
#38891=CARTESIAN_POINT('Ctrl Pts',(-3.43817673987435,-0.433127500149091,
2.34212073872434));
#38892=CARTESIAN_POINT('Ctrl Pts',(-1.53268946892128,-3.10797698807607,
2.49925925223786));
#38893=CARTESIAN_POINT('Ctrl Pts',(1.7493988709872,-2.99136460950407,2.65639776575137));
#38894=CARTESIAN_POINT('Ctrl Pts',(3.46024629894863,-0.188026617557356,
2.81353627926488));
#38895=CARTESIAN_POINT('Ctrl Pts',(2.06323722577413,2.78418938435949,2.97067479277839));
#38896=CARTESIAN_POINT('Ctrl Pts',(-1.18688998506621,3.25575653825361,3.12781330629191));
#38897=CARTESIAN_POINT('Ctrl Pts',(-3.3709995165217,0.803131807227777,3.28495181980542));
#38898=CARTESIAN_POINT('Ctrl Pts',(-2.52741049074122,-2.37083416635282,
3.44209033331894));
#38899=CARTESIAN_POINT('Ctrl Pts',(0.586198762341201,-3.41541058398195,
3.59922884683245));
#38900=CARTESIAN_POINT('Ctrl Pts',(3.17330745213002,-1.3924001776803,3.75636736034597));
#38901=CARTESIAN_POINT('Ctrl Pts',(2.91027678633445,1.88120904397026,3.91350587385948));
#38902=CARTESIAN_POINT('Ctrl Pts',(0.0333505152943699,3.46519064195013,
4.07064438737299));
#38903=CARTESIAN_POINT('Ctrl Pts',(-2.87352987075533,1.93687493734171,4.22778290088651));
#38904=CARTESIAN_POINT('Ctrl Pts',(-3.19951927885268,-1.33106529716661,
4.38492141440001));
#38905=CARTESIAN_POINT('Ctrl Pts',(-0.651826904677972,-3.40349528097662,
4.54205992791353));
#38906=CARTESIAN_POINT('Ctrl Pts',(2.48131063733581,-2.41904029776201,4.69919844142705));
#38907=CARTESIAN_POINT('Ctrl Pts',(3.38583301773356,0.738101088738959,4.85633695494055));
#38908=CARTESIAN_POINT('Ctrl Pts',(1.24933397805696,3.23230924456058,5.01347546845408));
#38909=CARTESIAN_POINT('Ctrl Pts',(-2.00926747133911,2.82338496663079,5.17061398196758));
#38910=CARTESIAN_POINT('Ctrl Pts',(-3.46322427730269,-0.12139211787978,
5.3277524954811));
#38911=CARTESIAN_POINT('Ctrl Pts',(-1.80664989208085,-2.95713959911133,
5.48489100899462));
#38912=CARTESIAN_POINT('Ctrl Pts',(1.47258603363221,-3.13690114838409,5.64202952250812));
#38913=CARTESIAN_POINT('Ctrl Pts',(3.4292033754596,-0.499222045701823,5.79916803602164));
#38914=CARTESIAN_POINT('Ctrl Pts',(2.30584575575073,2.58683857089803,5.95630654953515));
#38915=CARTESIAN_POINT('Ctrl Pts',(-0.888531402702859,3.34950300605675,
6.11344506304867));
#38916=CARTESIAN_POINT('Ctrl Pts',(-3.28486476693535,1.10377620199891,6.27058357656218));
#38917=CARTESIAN_POINT('Ctrl Pts',(-2.73086240406331,-2.13331876928079,
6.4277220900757));
#38918=CARTESIAN_POINT('Ctrl Pts',(0.275892655912234,-3.45435112336383,
6.5848606035892));
#38919=CARTESIAN_POINT('Ctrl Pts',(3.03485183459055,-1.67282180255638,6.74199911710273));
#38920=CARTESIAN_POINT('Ctrl Pts',(3.06802702248421,1.6111699572782,6.89913763061623));
#38921=CARTESIAN_POINT('Ctrl Pts',(0.345621576330127,3.44807252913389,7.05627614412975));
#38922=CARTESIAN_POINT('Ctrl Pts',(-2.68720751132516,2.18805261171336,7.21341465764325));
#38923=CARTESIAN_POINT('Ctrl Pts',(-3.30649300260574,-1.03718969811004,
7.37055317115678));
#38924=CARTESIAN_POINT('Ctrl Pts',(-0.956017138014702,-3.33086920560938,
7.52769168467029));
#38925=CARTESIAN_POINT('Ctrl Pts',(2.25311553735071,-2.63289362024357,7.68483019818381));
#38926=CARTESIAN_POINT('Ctrl Pts',(3.43858888024395,0.429842977951538,7.84196871169731));
#38927=CARTESIAN_POINT('Ctrl Pts',(1.53565755714059,3.10651158777771,7.99910722521083));
#38928=CARTESIAN_POINT('Ctrl Pts',(-1.74654067132524,2.99303427005181,8.15624573872433));
#38929=CARTESIAN_POINT('Ctrl Pts',(-3.46006514069016,0.191331803382343,
8.31338425223787));
#38930=CARTESIAN_POINT('Ctrl Pts',(-2.06589572612039,-2.78221724805058,
8.47052276575136));
#38931=CARTESIAN_POINT('Ctrl Pts',(1.183779392948,-3.25688886436581,8.62766127926489));
#38932=CARTESIAN_POINT('Ctrl Pts',(3.37023102179748,-0.806351310370959,
8.7847997927784));
#38933=CARTESIAN_POINT('Ctrl Pts',(2.52967359714463,2.36841856552378,8.94193830629191));
#38934=CARTESIAN_POINT('Ctrl Pts',(-0.582935293544439,3.41596954985013,
9.09907681980542));
#38935=CARTESIAN_POINT('Ctrl Pts',(-3.17197740603666,1.3954296219005,9.25621533331893));
#38936=CARTESIAN_POINT('Ctrl Pts',(-2.91206965945989,-1.87842613074489,
9.41335384683245));
#38937=CARTESIAN_POINT('Ctrl Pts',(-0.0366657672894424,-3.46516125435096,
9.57049236034596));
#38938=CARTESIAN_POINT('Ctrl Pts',(2.8716885037831,-1.93961114588268,9.72763087385947));
#38939=CARTESIAN_POINT('Ctrl Pts',(3.20077001198978,1.32799366090119,9.88476938737299));
#38940=CARTESIAN_POINT('Ctrl Pts',(0.655114493273841,3.40289939669598,10.0419079008865));
#38941=CARTESIAN_POINT('Ctrl Pts',(-2.47906919875826,2.42135526672317,10.1990464144));
#38942=CARTESIAN_POINT('Ctrl Pts',(-3.3864019310671,-0.734763106864168,
10.3561849279135));
#38943=CARTESIAN_POINT('Ctrl Pts',(-1.25267830620767,-3.23131219035953,
10.513323441427));
#38944=CARTESIAN_POINT('Ctrl Pts',(2.00706204302524,-2.82492459714601,10.6704619549406));
#38945=CARTESIAN_POINT('Ctrl Pts',(3.46239353138226,0.117358798249391,10.8276004684541));
#38946=CARTESIAN_POINT('Ctrl Pts',(1.81131357477516,2.9568147670617,10.9847389819676));
#38947=CARTESIAN_POINT('Ctrl Pts',(-1.47339811761136,3.13548357068097,11.1418774954811));
#38948=CARTESIAN_POINT('Ctrl Pts',(-2.77050414434575,1.38461669033425,11.2466365044901));
#38949=CARTESIAN_POINT('Ctrl Pts',(-2.91090525077877,0.426608275808828,
11.2990160089946));
#38950=CARTESIAN_POINT('Ctrl Pts',(1.59774743137964,-2.24059110187414,-0.219489327336925));
#38951=CARTESIAN_POINT('Ctrl Pts',(2.33514866714022,-1.71475623207252,-0.167109822832421));
#38952=CARTESIAN_POINT('Ctrl Pts',(3.23863136773739,0.11226788144075,-0.0623508138234118));
#38953=CARTESIAN_POINT('Ctrl Pts',(1.6876604910601,2.76982094937113,0.0947876996901019));
#38954=CARTESIAN_POINT('Ctrl Pts',(-1.38044412748324,2.93181193130462,0.251926213203615));
#38955=CARTESIAN_POINT('Ctrl Pts',(-3.2079816177237,0.464474356210045,0.409064726717129));
#38956=CARTESIAN_POINT('Ctrl Pts',(-2.15460694798876,-2.42206010021071,
0.566203240230643));
#38957=CARTESIAN_POINT('Ctrl Pts',(0.834144210720117,-3.13213929648004,
0.723341753744155));
#38958=CARTESIAN_POINT('Ctrl Pts',(3.07359869399491,-1.02960715343621,0.880480267257669));
#38959=CARTESIAN_POINT('Ctrl Pts',(2.55252127926951,1.99796636155783,1.03761878077118));
#38960=CARTESIAN_POINT('Ctrl Pts',(-0.261157599233816,3.2308943271893,1.19475729428469));
#38961=CARTESIAN_POINT('Ctrl Pts',(-2.84026054414775,1.56203972461538,1.35189580779821));
#38962=CARTESIAN_POINT('Ctrl Pts',(-2.86836128896387,-1.50981857631063,
1.50903432131172));
#38963=CARTESIAN_POINT('Ctrl Pts',(-0.320209305227662,-3.22559586930712,
1.66617283482524));
#38964=CARTESIAN_POINT('Ctrl Pts',(2.51553994814305,-2.04428172839443,1.82331134833875));
#38965=CARTESIAN_POINT('Ctrl Pts',(3.09193171078347,0.973131394588079,1.98044986185226));
#38966=CARTESIAN_POINT('Ctrl Pts',(0.891272025644291,3.1165132590083,2.13758837536578));
#38967=CARTESIAN_POINT('Ctrl Pts',(-2.10989267602029,2.4607676867899,2.29472688887929));
#38968=CARTESIAN_POINT('Ctrl Pts',(-3.21603530707201,-0.405143027346019,
2.4518654023928));
#38969=CARTESIAN_POINT('Ctrl Pts',(-1.43366203071003,-2.90716984129947,
2.60900391590632));
#38970=CARTESIAN_POINT('Ctrl Pts',(1.63636978576396,-2.79809181678146,2.76614242941983));
#38971=CARTESIAN_POINT('Ctrl Pts',(3.23667894658341,-0.175878172207005,
2.92328094293335));
#38972=CARTESIAN_POINT('Ctrl Pts',(1.92993096835312,2.60430223316632,3.08041945644686));
#38973=CARTESIAN_POINT('Ctrl Pts',(-1.11020473535129,3.04540131890859,3.23755796996037));
#38974=CARTESIAN_POINT('Ctrl Pts',(-3.15319842040834,0.751241266431068,
3.39469648347389));
#38975=CARTESIAN_POINT('Ctrl Pts',(-2.36411388612472,-2.21765399601942,
3.5518349969874));
#38976=CARTESIAN_POINT('Ctrl Pts',(0.548324318173406,-3.19474007803184,
3.70897351050091));
#38977=CARTESIAN_POINT('Ctrl Pts',(2.96827928823051,-1.30243686459143,3.86611202401443));
#38978=CARTESIAN_POINT('Ctrl Pts',(2.72224309752783,1.75966367151117,4.02325053752794));
#38979=CARTESIAN_POINT('Ctrl Pts',(0.0311957304148393,3.24130383438475,
4.18038905104146));
#38980=CARTESIAN_POINT('Ctrl Pts',(-2.68787040907414,1.81173297801481,4.33752756455496));
#38981=CARTESIAN_POINT('Ctrl Pts',(-2.99279756247315,-1.24506484557935,
4.49466607806848));
#38982=CARTESIAN_POINT('Ctrl Pts',(-0.609712210321215,-3.18359462564273,
4.65180459158199));
#38983=CARTESIAN_POINT('Ctrl Pts',(2.32099255542547,-2.26274551758992,4.80894310509551));
#38984=CARTESIAN_POINT('Ctrl Pts',(3.16707352551029,0.69041219843154,4.96608161860902));
#38985=CARTESIAN_POINT('Ctrl Pts',(1.16861420681437,3.02346896054623,5.12322013212254));
#38986=CARTESIAN_POINT('Ctrl Pts',(-1.87944821283798,2.64096537936348,5.28035864563605));
#38987=CARTESIAN_POINT('Ctrl Pts',(-3.23946451703395,-0.113548943710187,
5.43749715914956));
#38988=CARTESIAN_POINT('Ctrl Pts',(-1.68992180450333,-2.76607809260859,
5.59463567266307));
#38989=CARTESIAN_POINT('Ctrl Pts',(1.37744189294803,-2.93422520459686,5.75177418617659));
#38990=CARTESIAN_POINT('Ctrl Pts',(3.20764171390784,-0.466967188284919,
5.9089126996901));
#38991=CARTESIAN_POINT('Ctrl Pts',(2.15686450238375,2.41970230361335,6.06605121320362));
#38992=CARTESIAN_POINT('Ctrl Pts',(-0.831123173336083,3.13309080469669,
6.22318972671712));
#38993=CARTESIAN_POINT('Ctrl Pts',(-3.07262885787747,1.03246095396017,6.38032824023064));
#38994=CARTESIAN_POINT('Ctrl Pts',(-2.55442072199701,-1.99548452634149,
6.53746675374416));
#38995=CARTESIAN_POINT('Ctrl Pts',(0.258067164519323,-3.23116465972251,
6.69460526725767));
#38996=CARTESIAN_POINT('Ctrl Pts',(2.83876932171097,-1.56474038029172,6.85174378077119));
#38997=CARTESIAN_POINT('Ctrl Pts',(2.86980105267096,1.50707187568543,7.00888229428469));
#38998=CARTESIAN_POINT('Ctrl Pts',(0.323290882482136,3.22529172698812,7.1660208077982));
#38999=CARTESIAN_POINT('Ctrl Pts',(-2.51358638246349,2.04668200194341,7.32315932131173));
#39000=CARTESIAN_POINT('Ctrl Pts',(-3.09285968799709,-0.970176620232505,
7.48029783482524));
#39001=CARTESIAN_POINT('Ctrl Pts',(-0.89424863892644,-3.11566093861428,
7.63743634833875));
#39002=CARTESIAN_POINT('Ctrl Pts',(2.10754119617984,-2.46278172505391,7.79457486185227));
#39003=CARTESIAN_POINT('Ctrl Pts',(3.21642081895241,0.402070718924034,7.95171337536577));
#39004=CARTESIAN_POINT('Ctrl Pts',(1.43643835002984,2.90579912086969,8.1088518888793));
#39005=CARTESIAN_POINT('Ctrl Pts',(-1.63369625507517,2.79965360015637,8.2659904023928));
#39006=CARTESIAN_POINT('Ctrl Pts',(-3.23650949300394,0.178969809174445,
8.42312891590632));
#39007=CARTESIAN_POINT('Ctrl Pts',(-1.93241770234741,-2.6024575170625,8.58026742941983));
#39008=CARTESIAN_POINT('Ctrl Pts',(1.10729511934404,-3.04646048515613,8.73740594293334));
#39009=CARTESIAN_POINT('Ctrl Pts',(3.15247957831459,-0.75425275669555,8.89454445644686));
#39010=CARTESIAN_POINT('Ctrl Pts',(2.36623077267467,2.21539446774564,9.05168296996036));
#39011=CARTESIAN_POINT('Ctrl Pts',(-0.54527170288688,3.19526292897974,9.20882148347389));
#39012=CARTESIAN_POINT('Ctrl Pts',(-2.96703517673773,1.30527057568604,9.36595999698739));
#39013=CARTESIAN_POINT('Ctrl Pts',(-2.72392013268591,-1.75706056298405,
9.52309851050092));
#39014=CARTESIAN_POINT('Ctrl Pts',(-0.0342967831746755,-3.24127634552548,
9.68023702401442));
#39015=CARTESIAN_POINT('Ctrl Pts',(2.68614801326846,-1.81429239945851,9.83737553752795));
#39016=CARTESIAN_POINT('Ctrl Pts',(2.99396748543899,1.24219166847781,9.99451405104144));
#39017=CARTESIAN_POINT('Ctrl Pts',(0.612787387020777,3.18303724158995,10.151652564555));
#39018=CARTESIAN_POINT('Ctrl Pts',(-2.31889593673789,2.2649109158452,10.3087910780685));
#39019=CARTESIAN_POINT('Ctrl Pts',(-3.16760568121541,-0.687289884375024,
10.465929591582));
#39020=CARTESIAN_POINT('Ctrl Pts',(-1.17174245711238,-3.02253632625886,
10.6230681050955));
#39021=CARTESIAN_POINT('Ctrl Pts',(1.8773852777822,-2.64240553397781,10.780206618609));
#39022=CARTESIAN_POINT('Ctrl Pts',(3.23868744580887,0.109776217839061,10.9373451321225));
#39023=CARTESIAN_POINT('Ctrl Pts',(1.69428416552798,2.76577424803644,11.0944836456361));
#39024=CARTESIAN_POINT('Ctrl Pts',(-1.37820150798437,2.93289921693286,11.2516221591496));
#39025=CARTESIAN_POINT('Ctrl Pts',(-2.59150119982806,1.29515627025004,11.3563811681586));
#39026=CARTESIAN_POINT('Ctrl Pts',(-2.72283095673203,0.399045011671044,
11.4087606726631));
#39027=CARTESIAN_POINT('Ctrl Pts',(1.48738611075532,-2.08582659521589,-0.109744663668464));
#39028=CARTESIAN_POINT('Ctrl Pts',(2.17385277913045,-1.59631275433404,-0.0573651591639592));
#39029=CARTESIAN_POINT('Ctrl Pts',(3.01492915564857,0.104513194175331,0.0473938498450494));
#39030=CARTESIAN_POINT('Ctrl Pts',(1.57108859934498,2.57850091226017,0.204532363358563));
#39031=CARTESIAN_POINT('Ctrl Pts',(-1.28509261324199,2.72930267971312,0.361670876872076));
#39032=CARTESIAN_POINT('Ctrl Pts',(-2.98639647797178,0.432391686358259,
0.51880939038559));
#39033=CARTESIAN_POINT('Ctrl Pts',(-2.00578163083517,-2.25476097267596,
0.675947903899103));
#39034=CARTESIAN_POINT('Ctrl Pts',(0.776527309025778,-2.9157928187139,0.833086417412617));
#39035=CARTESIAN_POINT('Ctrl Pts',(2.86129579537873,-0.958489026161636,
0.99022493092613));
#39036=CARTESIAN_POINT('Ctrl Pts',(2.37621079754423,1.85996069064019,1.14736344443964));
#39037=CARTESIAN_POINT('Ctrl Pts',(-0.243118642026661,3.00772653624605,
1.30450195795316));
#39038=CARTESIAN_POINT('Ctrl Pts',(-2.64407502795598,1.45414484493007,1.46164047146667));
#39039=CARTESIAN_POINT('Ctrl Pts',(-2.67023476805036,-1.40553077167252,
1.61877898498018));
#39040=CARTESIAN_POINT('Ctrl Pts',(-0.298091465381954,-3.00279405911757,
1.7759174984937));
#39041=CARTESIAN_POINT('Ctrl Pts',(2.34178388050189,-1.90307691288803,1.93305601200721));
#39042=CARTESIAN_POINT('Ctrl Pts',(2.87836249441012,0.905914221373807,2.09019452552073));
#39043=CARTESIAN_POINT('Ctrl Pts',(0.829709130374474,2.90124611962672,2.24733303903424));
#39044=CARTESIAN_POINT('Ctrl Pts',(-1.96415591091712,2.2907949074068,2.40447155254775));
#39045=CARTESIAN_POINT('Ctrl Pts',(-2.99389387426969,-0.37715855454295,
2.56161006606126));
#39046=CARTESIAN_POINT('Ctrl Pts',(-1.33463459249878,-2.70636269452286,
2.71874857957478));
#39047=CARTESIAN_POINT('Ctrl Pts',(1.52334070054072,-2.60481902405885,2.87588709308829));
#39048=CARTESIAN_POINT('Ctrl Pts',(3.01311159421818,-0.163729726856653,
3.03302560660181));
#39049=CARTESIAN_POINT('Ctrl Pts',(1.79662471093212,2.42441508197314,3.19016412011532));
#39050=CARTESIAN_POINT('Ctrl Pts',(-1.03351948563637,2.83504609956357,3.34730263362884));
#39051=CARTESIAN_POINT('Ctrl Pts',(-2.93539732429499,0.699350725634357,
3.50444114714234));
#39052=CARTESIAN_POINT('Ctrl Pts',(-2.20081728150821,-2.06447382568602,
3.66157966065586));
#39053=CARTESIAN_POINT('Ctrl Pts',(0.510449874005612,-2.97406957208172,
3.81871817416937));
#39054=CARTESIAN_POINT('Ctrl Pts',(2.763251124331,-1.21247355150257,3.97585668768289));
#39055=CARTESIAN_POINT('Ctrl Pts',(2.5342094087212,1.63811829905208,4.1329952011964));
#39056=CARTESIAN_POINT('Ctrl Pts',(0.029040945535309,3.01741702681936,4.29013371470992));
#39057=CARTESIAN_POINT('Ctrl Pts',(-2.50221094739296,1.68659101868791,4.44727222822342));
#39058=CARTESIAN_POINT('Ctrl Pts',(-2.78607584609361,-1.1590643939921,4.60441074173694));
#39059=CARTESIAN_POINT('Ctrl Pts',(-0.56759751596446,-2.96369397030884,
4.76154925525046));
#39060=CARTESIAN_POINT('Ctrl Pts',(2.16067447351513,-2.10645073741783,4.91868776876396));
#39061=CARTESIAN_POINT('Ctrl Pts',(2.94831403328702,0.642723308124124,5.07582628227749));
#39062=CARTESIAN_POINT('Ctrl Pts',(1.08789443557179,2.81462867653188,5.23296479579099));
#39063=CARTESIAN_POINT('Ctrl Pts',(-1.74962895433684,2.45854579209617,5.39010330930451));
#39064=CARTESIAN_POINT('Ctrl Pts',(-3.01570475676522,-0.105705769540595,
5.54724182281802));
#39065=CARTESIAN_POINT('Ctrl Pts',(-1.57319371692581,-2.57501658610585,
5.70438033633154));
#39066=CARTESIAN_POINT('Ctrl Pts',(1.28229775226384,-2.73154926080963,5.86151884984505));
#39067=CARTESIAN_POINT('Ctrl Pts',(2.98608005235609,-0.434712330868017,
6.01865736335856));
#39068=CARTESIAN_POINT('Ctrl Pts',(2.00788324901678,2.25256603632868,6.17579587687208));
#39069=CARTESIAN_POINT('Ctrl Pts',(-0.773714943969305,2.91667860333663,
6.33293439038559));
#39070=CARTESIAN_POINT('Ctrl Pts',(-2.86039294881959,0.961145705921419,
6.4900729038991));
#39071=CARTESIAN_POINT('Ctrl Pts',(-2.37797903993071,-1.85765028340219,
6.64721141741262));
#39072=CARTESIAN_POINT('Ctrl Pts',(0.240241673126412,-3.0079781960812,6.80434993092612));
#39073=CARTESIAN_POINT('Ctrl Pts',(2.64268680883139,-1.45665895802706,6.96148844443965));
#39074=CARTESIAN_POINT('Ctrl Pts',(2.67157508285772,1.40297379409266,7.11862695795316));
#39075=CARTESIAN_POINT('Ctrl Pts',(0.300960188634146,3.00251092484234,7.27576547146667));
#39076=CARTESIAN_POINT('Ctrl Pts',(-2.33996525360183,1.90531139217345,7.43290398498018));
#39077=CARTESIAN_POINT('Ctrl Pts',(-2.87922637338843,-0.903163542354968,
7.5900424984937));
#39078=CARTESIAN_POINT('Ctrl Pts',(-0.832480139838179,-2.90045267161919,
7.74718101200721));
#39079=CARTESIAN_POINT('Ctrl Pts',(1.96196685500896,-2.29266982986425,7.90431952552073));
#39080=CARTESIAN_POINT('Ctrl Pts',(2.99425275766087,0.37429845989653,8.06145803903424));
#39081=CARTESIAN_POINT('Ctrl Pts',(1.33721914291908,2.70508665396167,8.21859655254775));
#39082=CARTESIAN_POINT('Ctrl Pts',(-1.5208518388251,2.60627293026094,8.37573506606126));
#39083=CARTESIAN_POINT('Ctrl Pts',(-3.01295384531772,0.166607814966547,
8.53287357957478));
#39084=CARTESIAN_POINT('Ctrl Pts',(-1.79893967857444,-2.42269778607442,
8.69001209308829));
#39085=CARTESIAN_POINT('Ctrl Pts',(1.03081084574009,-2.83603210594645,8.8471506066018));
#39086=CARTESIAN_POINT('Ctrl Pts',(2.9347281348317,-0.702154203020143,9.00428912011532));
#39087=CARTESIAN_POINT('Ctrl Pts',(2.20278794820472,2.06237036996751,9.16142763362883));
#39088=CARTESIAN_POINT('Ctrl Pts',(-0.507608112229325,2.97455630810935,
9.31856614714235));
#39089=CARTESIAN_POINT('Ctrl Pts',(-2.7620929474388,1.21511152947157,9.47570466065586));
#39090=CARTESIAN_POINT('Ctrl Pts',(-2.53577060591194,-1.63569499522321,
9.63284317416937));
#39091=CARTESIAN_POINT('Ctrl Pts',(-0.0319277990599106,-3.0173914367,9.78998168768289));
#39092=CARTESIAN_POINT('Ctrl Pts',(2.50060752275382,-1.68897365303435,9.94712020119639));
#39093=CARTESIAN_POINT('Ctrl Pts',(2.78716495888821,1.15638967605443,10.1042587147099));
#39094=CARTESIAN_POINT('Ctrl Pts',(0.570460280767717,2.96317508648391,10.2613972282234));
#39095=CARTESIAN_POINT('Ctrl Pts',(-2.15872267471752,2.10846656496723,10.4185357417369));
#39096=CARTESIAN_POINT('Ctrl Pts',(-2.94880943136371,-0.639816661885883,
10.5756742552505));
#39097=CARTESIAN_POINT('Ctrl Pts',(-1.09080660801709,-2.8137604621582,10.732812768764));
#39098=CARTESIAN_POINT('Ctrl Pts',(1.74770851253917,-2.4598864708096,10.8899512822775));
#39099=CARTESIAN_POINT('Ctrl Pts',(3.01498136023548,0.102193637428725,11.047089795791));
#39100=CARTESIAN_POINT('Ctrl Pts',(1.57725475628079,2.57473372901119,11.2042283093045));
#39101=CARTESIAN_POINT('Ctrl Pts',(-1.28300489835739,2.73031486318474,11.361366822818));
#39102=CARTESIAN_POINT('Ctrl Pts',(-2.41249825531037,1.20569585016584,11.466125831827));
#39103=CARTESIAN_POINT('Ctrl Pts',(-2.53475666268528,0.371481747533259,
11.5185053363315));
#39104=CARTESIAN_POINT('Ctrl Pts',(1.37702479013101,-1.93106208855765,-2.4980018054066E-15));
#39105=CARTESIAN_POINT('Ctrl Pts',(2.01255689112068,-1.47786927659557,0.052379504504502));
#39106=CARTESIAN_POINT('Ctrl Pts',(2.79122694355976,0.0967585069099138,
0.157138513513511));
#39107=CARTESIAN_POINT('Ctrl Pts',(1.45451670762985,2.3871808751492,0.314277027027025));
#39108=CARTESIAN_POINT('Ctrl Pts',(-1.18974109900074,2.52679342812162,0.471415540540538));
#39109=CARTESIAN_POINT('Ctrl Pts',(-2.76481133821986,0.40030901650647,0.628554054054051));
#39110=CARTESIAN_POINT('Ctrl Pts',(-1.85695631368159,-2.0874618451412,0.785692567567565));
#39111=CARTESIAN_POINT('Ctrl Pts',(0.718910407331439,-2.69944634094777,
0.942831081081078));
#39112=CARTESIAN_POINT('Ctrl Pts',(2.64899289676255,-0.887370898887054,
1.09996959459459));
#39113=CARTESIAN_POINT('Ctrl Pts',(2.19990031581894,1.72195501972256,1.25710810810811));
#39114=CARTESIAN_POINT('Ctrl Pts',(-0.225079684819506,2.78455874530281,
1.41424662162162));
#39115=CARTESIAN_POINT('Ctrl Pts',(-2.44788951176421,1.34624996524475,1.57138513513514));
#39116=CARTESIAN_POINT('Ctrl Pts',(-2.47210824713685,-1.30124296703442,
1.72852364864864));
#39117=CARTESIAN_POINT('Ctrl Pts',(-0.275973625536248,-2.77999224892802,
1.88566216216216));
#39118=CARTESIAN_POINT('Ctrl Pts',(2.16802781286073,-1.76187209738162,2.04280067567567));
#39119=CARTESIAN_POINT('Ctrl Pts',(2.66479327803676,0.838697048159531,2.19993918918919));
#39120=CARTESIAN_POINT('Ctrl Pts',(0.76814623510466,2.68597898024514,2.3570777027027));
#39121=CARTESIAN_POINT('Ctrl Pts',(-1.81841914581395,2.1208221280237,2.51421621621621));
#39122=CARTESIAN_POINT('Ctrl Pts',(-2.77175244146736,-0.349174081739879,
2.67135472972972));
#39123=CARTESIAN_POINT('Ctrl Pts',(-1.23560715428754,-2.50555554774625,
2.82849324324324));
#39124=CARTESIAN_POINT('Ctrl Pts',(1.41031161531747,-2.41154623133624,2.98563175675675));
#39125=CARTESIAN_POINT('Ctrl Pts',(2.78954424185296,-0.151581281506301,
3.14277027027027));
#39126=CARTESIAN_POINT('Ctrl Pts',(1.66331845351111,2.24452793077997,3.29990878378378));
#39127=CARTESIAN_POINT('Ctrl Pts',(-0.956834235921451,2.62469088021855,
3.45704729729729));
#39128=CARTESIAN_POINT('Ctrl Pts',(-2.71759622818163,0.647460184837647,
3.61418581081081));
#39129=CARTESIAN_POINT('Ctrl Pts',(-2.03752067689171,-1.91129365535261,
3.77132432432432));
#39130=CARTESIAN_POINT('Ctrl Pts',(0.47257542983782,-2.75339906613161,3.92846283783783));
#39131=CARTESIAN_POINT('Ctrl Pts',(2.55822296043148,-1.12251023841371,4.08560135135135));
#39132=CARTESIAN_POINT('Ctrl Pts',(2.34617571991457,1.51657292659299,4.24273986486486));
#39133=CARTESIAN_POINT('Ctrl Pts',(0.0268861606557786,2.79353021925399,
4.39987837837838));
#39134=CARTESIAN_POINT('Ctrl Pts',(-2.31655148571177,1.56144905936101,4.55701689189189));
#39135=CARTESIAN_POINT('Ctrl Pts',(-2.57935412971408,-1.07306394240484,
4.7141554054054));
#39136=CARTESIAN_POINT('Ctrl Pts',(-0.525482821607704,-2.74379331497496,
4.87129391891892));
#39137=CARTESIAN_POINT('Ctrl Pts',(2.00035639160479,-1.95015595724574,5.02843243243243));
#39138=CARTESIAN_POINT('Ctrl Pts',(2.72955454106374,0.595034417816705,5.18557094594594));
#39139=CARTESIAN_POINT('Ctrl Pts',(1.0071746643292,2.60578839251754,5.34270945945947));
#39140=CARTESIAN_POINT('Ctrl Pts',(-1.61980969583571,2.27612620482886,5.49984797297296));
#39141=CARTESIAN_POINT('Ctrl Pts',(-2.79194499649648,-0.0978625953710016,
5.6569864864865));
#39142=CARTESIAN_POINT('Ctrl Pts',(-1.45646562934828,-2.38395507960311,
5.81412499999999));
#39143=CARTESIAN_POINT('Ctrl Pts',(1.18715361157964,-2.5288733170224,5.97126351351352));
#39144=CARTESIAN_POINT('Ctrl Pts',(2.76451839080433,-0.402457473451116,
6.12840202702702));
#39145=CARTESIAN_POINT('Ctrl Pts',(1.8589019956498,2.08542976904401,6.28554054054054));
#39146=CARTESIAN_POINT('Ctrl Pts',(-0.716306714602523,2.70026640197657,
6.44267905405405));
#39147=CARTESIAN_POINT('Ctrl Pts',(-2.64815703976171,0.889830457882673,
6.59981756756756));
#39148=CARTESIAN_POINT('Ctrl Pts',(-2.20153735786441,-1.71981604046289,
6.75695608108108));
#39149=CARTESIAN_POINT('Ctrl Pts',(0.222416181733502,-2.78479173243988,
6.91409459459459));
#39150=CARTESIAN_POINT('Ctrl Pts',(2.4466042959518,-1.34857753576241,7.0712331081081));
#39151=CARTESIAN_POINT('Ctrl Pts',(2.47334911304448,1.29887571249989,7.22837162162162));
#39152=CARTESIAN_POINT('Ctrl Pts',(0.278629494786153,2.77973012269657,7.38551013513513));
#39153=CARTESIAN_POINT('Ctrl Pts',(-2.16634412474015,1.76394078240349,7.54264864864865));
#39154=CARTESIAN_POINT('Ctrl Pts',(-2.66559305877978,-0.83615046447743,
7.69978716216215));
#39155=CARTESIAN_POINT('Ctrl Pts',(-0.770711640749916,-2.68524440462409,
7.85692567567567));
#39156=CARTESIAN_POINT('Ctrl Pts',(1.81639251383808,-2.12255793467458,8.01406418918919));
#39157=CARTESIAN_POINT('Ctrl Pts',(2.77208469636934,0.346526200869026,8.1712027027027));
#39158=CARTESIAN_POINT('Ctrl Pts',(1.23799993580832,2.50437418705365,8.32834121621622));
#39159=CARTESIAN_POINT('Ctrl Pts',(-1.40800742257503,2.4128922603655,8.48547972972973));
#39160=CARTESIAN_POINT('Ctrl Pts',(-2.78939819763151,0.154245820758651,
8.64261824324324));
#39161=CARTESIAN_POINT('Ctrl Pts',(-1.66546165480147,-2.24293805508635,
8.79975675675676));
#39162=CARTESIAN_POINT('Ctrl Pts',(0.954326572136137,-2.62560372673677,
8.95689527027026));
#39163=CARTESIAN_POINT('Ctrl Pts',(2.71697669134881,-0.650055649344734,
9.11403378378378));
#39164=CARTESIAN_POINT('Ctrl Pts',(2.03934512373477,1.90934627218937,9.2711722972973));
#39165=CARTESIAN_POINT('Ctrl Pts',(-0.469944521571767,2.75384968723896,
9.42831081081079));
#39166=CARTESIAN_POINT('Ctrl Pts',(-2.55715071813987,1.12495248325711,9.58544932432433));
#39167=CARTESIAN_POINT('Ctrl Pts',(-2.34762107913798,-1.51432942746238,
9.74258783783783));
#39168=CARTESIAN_POINT('Ctrl Pts',(-0.0295588149451427,-2.79350652787453,
9.89972635135136));
#39169=CARTESIAN_POINT('Ctrl Pts',(2.31506703223917,-1.56365490661018,10.0568648648649));
#39170=CARTESIAN_POINT('Ctrl Pts',(2.58036243233743,1.07058768363104,10.2140033783784));
#39171=CARTESIAN_POINT('Ctrl Pts',(0.528133174514654,2.74331293137788,10.3711418918919));
#39172=CARTESIAN_POINT('Ctrl Pts',(-1.99854941269714,1.95202221408926,10.5282804054054));
#39173=CARTESIAN_POINT('Ctrl Pts',(-2.73001318151202,-0.59234343939674,
10.6854189189189));
#39174=CARTESIAN_POINT('Ctrl Pts',(-1.0098707589218,-2.60498459805753,10.8425574324324));
#39175=CARTESIAN_POINT('Ctrl Pts',(1.61803174729613,-2.2773674076414,10.999695945946));
#39176=CARTESIAN_POINT('Ctrl Pts',(2.79127527466209,0.0946110570183949,
11.1568344594594));
#39177=CARTESIAN_POINT('Ctrl Pts',(1.46022534703361,2.38369320998594,11.313972972973));
#39178=CARTESIAN_POINT('Ctrl Pts',(-1.1878082887304,2.52773050943662,11.4711114864865));
#39179=CARTESIAN_POINT('Ctrl Pts',(-2.23349531079268,1.11623543008163,11.5758704954955));
#39180=CARTESIAN_POINT('Ctrl Pts',(-2.34668236863853,0.343918483395475,
11.62825));
#39181=CARTESIAN_POINT('',(1.37702479013102,-1.93106208855765,0.));
#39182=CARTESIAN_POINT('Ctrl Pts',(1.37702479013101,-1.93106208855765,-2.4980018054066E-15));
#39183=CARTESIAN_POINT('Ctrl Pts',(2.01255689112068,-1.47786927659557,0.052379504504502));
#39184=CARTESIAN_POINT('Ctrl Pts',(2.79122694355976,0.0967585069099138,
0.157138513513511));
#39185=CARTESIAN_POINT('Ctrl Pts',(1.45451670762985,2.3871808751492,0.314277027027025));
#39186=CARTESIAN_POINT('Ctrl Pts',(-1.18974109900074,2.52679342812162,0.471415540540538));
#39187=CARTESIAN_POINT('Ctrl Pts',(-2.31615344009055,1.00603694073732,0.583793234229858));
#39188=CARTESIAN_POINT('Ctrl Pts',(-2.37458477423974,0.11510370689526,0.643791423414673));
#39189=CARTESIAN_POINT('Ctrl Pts',(-2.37366757034868,0.001844716469488,
0.651410108094984));
#39190=CARTESIAN_POINT('Ctrl Pts',(1.29197400994444,2.64783394680711,-2.46330733588707E-16));
#39191=CARTESIAN_POINT('Ctrl Pts',(1.37074936016223,2.60046826619745,-2.90204607120186E-16));
#39192=CARTESIAN_POINT('Ctrl Pts',(1.44700091320012,2.54930204226795,-5.92854700626308E-16));
#39193=CARTESIAN_POINT('Ctrl Pts',(1.5204041597113,2.49432533414619,-4.68375338513738E-16));
#39194=CARTESIAN_POINT('Ctrl Pts',(1.59876972116939,2.43563200920691,-3.1748808003354E-16));
#39195=CARTESIAN_POINT('Ctrl Pts',(1.67388955782072,2.37259497158855,9.42702435984343E-17));
#39196=CARTESIAN_POINT('Ctrl Pts',(1.74558455766593,2.30559334150577,2.91433543964104E-16));
#39197=CARTESIAN_POINT('Ctrl Pts',(1.78514524738377,2.26862241321206,4.00226572297347E-16));
#39198=CARTESIAN_POINT('Ctrl Pts',(1.82366240526687,2.23044382157621,2.41712413072573E-16));
#39199=CARTESIAN_POINT('Ctrl Pts',(1.86109995619813,2.19111823230724,2.56739074444567E-16));
#39200=CARTESIAN_POINT('Ctrl Pts',(1.87813922122651,2.17321964863167,2.63578284255041E-16));
#39201=CARTESIAN_POINT('Ctrl Pts',(1.89495840460327,2.15507923207588,-5.32738877742354E-17));
#39202=CARTESIAN_POINT('Ctrl Pts',(1.91153266312519,2.13672660521873,-9.0205620750794E-17));
#39203=CARTESIAN_POINT('Ctrl Pts',(1.97664662778045,2.0646261070319,-2.35296368099375E-16));
#39204=CARTESIAN_POINT('Ctrl Pts',(2.03804038590891,1.98919650283574,-3.72373475267393E-16));
#39205=CARTESIAN_POINT('Ctrl Pts',(2.09554796148623,1.91081666271006,-8.32667268468867E-17));
#39206=CARTESIAN_POINT('Ctrl Pts',(2.14343533270609,1.8455486617107,1.57476549926517E-16));
#39207=CARTESIAN_POINT('Ctrl Pts',(2.18862729734747,1.77823406218829,2.53857300975798E-16));
#39208=CARTESIAN_POINT('Ctrl Pts',(2.23100237945407,1.70908145885149,3.19189119579733E-16));
#39209=CARTESIAN_POINT('Ctrl Pts',(2.2495414778757,1.67882719489164,3.47771790218954E-16));
#39210=CARTESIAN_POINT('Ctrl Pts',(2.26754109313608,1.64822104628506,2.94521883274651E-16));
#39211=CARTESIAN_POINT('Ctrl Pts',(2.28498954152194,1.61728023964544,3.19189119579733E-16));
#39212=CARTESIAN_POINT('Ctrl Pts',(2.29543189661598,1.59876312668031,3.33951695310829E-16));
#39213=CARTESIAN_POINT('Ctrl Pts',(2.30567682494647,1.58012614919259,-6.61366324171955E-18));
#39214=CARTESIAN_POINT('Ctrl Pts',(2.31572165746038,1.56137299470242,-1.38777878078145E-17));
#39215=CARTESIAN_POINT('Ctrl Pts',(2.32292320728395,1.54792809393149,-1.90857347710862E-17));
#39216=CARTESIAN_POINT('Ctrl Pts',(2.33002152872364,1.53442403232929,-1.12870283643031E-16));
#39217=CARTESIAN_POINT('Ctrl Pts',(2.33700969851763,1.52087413145422,-1.11022302462516E-16));
#39218=CARTESIAN_POINT('Ctrl Pts',(2.38058260792534,1.43638725996736,-9.94996979838631E-17));
#39219=CARTESIAN_POINT('Ctrl Pts',(2.41994184512486,1.3499998824768,-3.77842799305168E-16));
#39220=CARTESIAN_POINT('Ctrl Pts',(2.45492973401008,1.26206183108408,-3.7470027081099E-16));
#39221=CARTESIAN_POINT('Ctrl Pts',(2.48961375478266,1.17488751738912,-3.71585035023886E-16));
#39222=CARTESIAN_POINT('Ctrl Pts',(2.52000223755862,1.08618841594484,-4.13121512185277E-16));
#39223=CARTESIAN_POINT('Ctrl Pts',(2.54589150534161,0.996296170221892,-3.7470027081099E-16));
#39224=CARTESIAN_POINT('Ctrl Pts',(2.57095558696702,0.909269120898709,-3.37503655671981E-16));
#39225=CARTESIAN_POINT('Ctrl Pts',(2.59180267862827,0.821123009321661,-1.98135956264892E-16));
#39226=CARTESIAN_POINT('Ctrl Pts',(2.60819974692058,0.732162501184589,-2.77555756156289E-16));
#39227=CARTESIAN_POINT('Ctrl Pts',(2.61796168819389,0.679200152025794,-3.24838075693952E-16));
#39228=CARTESIAN_POINT('Ctrl Pts',(2.62614545111416,0.625949276096869,-2.51374357035676E-17));
#39229=CARTESIAN_POINT('Ctrl Pts',(2.63269335080009,0.572476447093945,0.));
#39230=CARTESIAN_POINT('Ctrl Pts',(2.6352683765624,0.5514477327168,9.88554309620052E-18));
#39231=CARTESIAN_POINT('Ctrl Pts',(2.63759088070415,0.530377846603737,-5.43523939458827E-17));
#39232=CARTESIAN_POINT('Ctrl Pts',(2.63965388200594,0.50930758122065,-2.77555756156289E-17));
#39233=CARTESIAN_POINT('Ctrl Pts',(2.64834931960739,0.420497565576959,8.43485582923526E-17));
#39234=CARTESIAN_POINT('Ctrl Pts',(2.65245297898025,0.3315870178655,7.13394232030532E-17));
#39235=CARTESIAN_POINT('Ctrl Pts',(2.65178792227632,0.242870082265014,1.11022302462516E-16));
#39236=CARTESIAN_POINT('Ctrl Pts',(2.65141677862428,0.193360428001277,1.33167855834344E-16));
#39237=CARTESIAN_POINT('Ctrl Pts',(2.64955959473733,0.143911103160085,2.55410202784461E-16));
#39238=CARTESIAN_POINT('Ctrl Pts',(2.64617859082989,0.0945743399740305,
2.77555756156289E-16));
#39239=CARTESIAN_POINT('Ctrl Pts',(2.63998980161557,0.00426541509996067,
2.91350122435194E-16));
#39240=CARTESIAN_POINT('Ctrl Pts',(2.62869784498548,-0.0856678806083358,
1.22336690906674E-16));
#39241=CARTESIAN_POINT('Ctrl Pts',(2.61249699286393,-0.174890907412304,
1.94289029309402E-16));
#39242=CARTESIAN_POINT('Ctrl Pts',(2.59606370990205,-0.265394001643718,
2.67273655542046E-16));
#39243=CARTESIAN_POINT('Ctrl Pts',(2.57457910556097,-0.355167245076682,
-8.63540186836622E-17));
#39244=CARTESIAN_POINT('Ctrl Pts',(2.54820206281091,-0.443829678011398,
-1.94289029309402E-16));
#39245=CARTESIAN_POINT('Ctrl Pts',(2.5433159398537,-0.460253640057088,-2.14283072550056E-16));
#39246=CARTESIAN_POINT('Ctrl Pts',(2.53826078384047,-0.476642310793062,
2.54370247567095E-16));
#39247=CARTESIAN_POINT('Ctrl Pts',(2.53304532831965,-0.49296952041645,2.4980018054066E-16));
#39248=CARTESIAN_POINT('Ctrl Pts',(2.5060606614482,-0.577446189974434,2.26154741365496E-16));
#39249=CARTESIAN_POINT('Ctrl Pts',(2.47475215402615,-0.660408357948197,
3.47506847049484E-16));
#39250=CARTESIAN_POINT('Ctrl Pts',(2.43933604293942,-0.741555503604727,
2.77555756156289E-16));
#39251=CARTESIAN_POINT('Ctrl Pts',(2.40393876465244,-0.822659498618874,
2.07641862313994E-16));
#39252=CARTESIAN_POINT('Ctrl Pts',(2.3644375894048,-0.901951185787608,-1.23823437954767E-16));
#39253=CARTESIAN_POINT('Ctrl Pts',(2.32100582430644,-0.979100944080977,
-1.11022302462516E-16));
#39254=CARTESIAN_POINT('Ctrl Pts',(2.27823644108386,-1.05507408425856,-9.84163982743666E-17));
#39255=CARTESIAN_POINT('Ctrl Pts',(2.23165476456022,-1.1289707546069,2.53313632717541E-16));
#39256=CARTESIAN_POINT('Ctrl Pts',(2.18139506127574,-1.20043719637909,2.77555756156289E-16));
#39257=CARTESIAN_POINT('Ctrl Pts',(2.16608689289344,-1.2222045418435,2.84939454890925E-16));
#39258=CARTESIAN_POINT('Ctrl Pts',(2.15043733121093,-1.24374612322857,4.37114965090439E-17));
#39259=CARTESIAN_POINT('Ctrl Pts',(2.13444972694369,-1.26505107698559,0.));
#39260=CARTESIAN_POINT('Ctrl Pts',(2.12083931058568,-1.28318820912085,-3.72120586158607E-17));
#39261=CARTESIAN_POINT('Ctrl Pts',(2.10698390104784,-1.30115384375424,6.4814165885223E-17));
#39262=CARTESIAN_POINT('Ctrl Pts',(2.09288546869145,-1.31894102140198,5.55111512312578E-17));
#39263=CARTESIAN_POINT('Ctrl Pts',(2.08472665052523,-1.32923453095322,5.01274601200272E-17));
#39264=CARTESIAN_POINT('Ctrl Pts',(2.07648733901943,-1.33946704131009,1.07093663002969E-16));
#39265=CARTESIAN_POINT('Ctrl Pts',(2.06817568052718,-1.3496280615777,1.11022302462516E-16));
#39266=CARTESIAN_POINT('Ctrl Pts',(2.0141423836499,-1.41568388247163,1.36562011828508E-16));
#39267=CARTESIAN_POINT('Ctrl Pts',(1.95696807639868,-1.47883106712894,-2.06909962337776E-16));
#39268=CARTESIAN_POINT('Ctrl Pts',(1.89681447147471,-1.5387754276769,-2.22044604925031E-16));
#39269=CARTESIAN_POINT('Ctrl Pts',(1.83758356202805,-1.5978003023447,-2.36947097397864E-16));
#39270=CARTESIAN_POINT('Ctrl Pts',(1.77546340770889,-1.65372037608364,4.0590157288843E-16));
#39271=CARTESIAN_POINT('Ctrl Pts',(1.71058212140457,-1.70621256947127,4.44089209850063E-16));
#39272=CARTESIAN_POINT('Ctrl Pts',(1.64772546517897,-1.75706673624623,4.81085195985522E-16));
#39273=CARTESIAN_POINT('Ctrl Pts',(1.58227673616169,-1.80470390837557,2.58606592525932E-16));
#39274=CARTESIAN_POINT('Ctrl Pts',(1.5143365021986,-1.84878472647799,2.77555756156289E-16));
#39275=CARTESIAN_POINT('Ctrl Pts',(1.46963595841736,-1.87778722506477,2.90023153883192E-16));
#39276=CARTESIAN_POINT('Ctrl Pts',(1.42385657678108,-1.90524929950103,3.23574125955808E-17));
#39277=CARTESIAN_POINT('Ctrl Pts',(1.37702479013104,-1.93106208855763,5.55111512312578E-17));
#39278=CARTESIAN_POINT('Ctrl Pts',(0.261124777554701,2.92529416030267,11.058));
#39279=CARTESIAN_POINT('Ctrl Pts',(0.712806568001128,2.88599464153458,11.0335796606559));
#39280=CARTESIAN_POINT('Ctrl Pts',(1.15551467718148,2.74786827548953,11.0091593213117));
#39281=CARTESIAN_POINT('Ctrl Pts',(1.53904161881194,2.51335023952951,10.9847389819676));
#39282=CARTESIAN_POINT('Ctrl Pts',(2.36167356031087,2.01032944412425,10.9323594774631));
#39283=CARTESIAN_POINT('Ctrl Pts',(2.91203354584656,1.06384412118684,10.8799799729586));
#39284=CARTESIAN_POINT('Ctrl Pts',(2.94465829055491,0.100220893818898,10.8276004684541));
#39285=CARTESIAN_POINT('Ctrl Pts',(2.97728303526326,-0.863402333549067,
10.7752209639496));
#39286=CARTESIAN_POINT('Ctrl Pts',(2.49217253914424,-1.84416346534755,10.7228414594451));
#39287=CARTESIAN_POINT('Ctrl Pts',(1.70632723287924,-2.40227529678238,10.6704619549406));
#39288=CARTESIAN_POINT('Ctrl Pts',(0.92048192661426,-2.96038712821718,10.6180824504361));
#39289=CARTESIAN_POINT('Ctrl Pts',(-0.166098189796688,-3.09584965928835,
10.5657029459315));
#39290=CARTESIAN_POINT('Ctrl Pts',(-1.0650088521454,-2.74748941090806,10.513323441427));
#39291=CARTESIAN_POINT('Ctrl Pts',(-1.96391951449414,-2.39912916252775,
10.4609439369225));
#39292=CARTESIAN_POINT('Ctrl Pts',(-2.67516072278063,-1.56694613469595,
10.408564432418));
#39293=CARTESIAN_POINT('Ctrl Pts',(-2.87955920487239,-0.624834891848815,
10.3561849279135));
#39294=CARTESIAN_POINT('Ctrl Pts',(-2.92379628688831,-0.420937818389941,
10.3448486576389));
#39295=CARTESIAN_POINT('Ctrl Pts',(-2.94429281596354,-0.211891698741057,
10.3335123873642));
#39296=CARTESIAN_POINT('Ctrl Pts',(-2.94242444587263,-0.00248500551853048,
10.3221761170896));
#39297=CARTESIAN_POINT('Origin',(0.,0.,-1.84858989190501));
#39298=CARTESIAN_POINT('',(-1.37702479013099,-1.93106208855767,0.));
#39299=CARTESIAN_POINT('Ctrl Pts',(-1.37989654081094,-1.93326688769301,
3.07371315899641E-16));
#39300=CARTESIAN_POINT('Ctrl Pts',(-0.801986922861967,-2.34019513141193,
0.0475906520026623));
#39301=CARTESIAN_POINT('Ctrl Pts',(0.824868299691477,-2.62988338064349,
0.147626409229032));
#39302=CARTESIAN_POINT('Ctrl Pts',(2.66596861578497,-0.838738147770652,
0.30010727167911));
#39303=CARTESIAN_POINT('Ctrl Pts',(2.16631806184957,1.76615982799916,0.457442587350233));
#39304=CARTESIAN_POINT('Ctrl Pts',(-0.283824062622952,2.78024166545816,
0.614777903021357));
#39305=CARTESIAN_POINT('Ctrl Pts',(-2.10236314538525,1.54689613835291,0.745160337872953));
#39306=CARTESIAN_POINT('Ctrl Pts',(-2.3682722008076,0.381486792202907,0.823097667500842));
#39307=CARTESIAN_POINT('Ctrl Pts',(-2.36802324146013,0.000186122305323062,
0.848589891905023));
#39308=CARTESIAN_POINT('Origin',(0.,0.,0.));
#39309=CARTESIAN_POINT('Ctrl Pts',(-1.03908919352509,2.13201587949044,-0.329233991005384));
#39310=CARTESIAN_POINT('Ctrl Pts',(-1.74163600084562,1.78961280339009,-0.276788885781676));
#39311=CARTESIAN_POINT('Ctrl Pts',(-2.77044124913769,0.362429281341372,
-0.171898675334261));
#39312=CARTESIAN_POINT('Ctrl Pts',(-1.82442757362648,-2.1194917921021,-0.0145633596631371));
#39313=CARTESIAN_POINT('Ctrl Pts',(0.766254154833431,-2.68690713172521,
0.142771956007986));
#39314=CARTESIAN_POINT('Ctrl Pts',(2.66596861578497,-0.838738147770652,
0.30010727167911));
#39315=CARTESIAN_POINT('Ctrl Pts',(2.16631806184957,1.76615982799916,0.457442587350233));
#39316=CARTESIAN_POINT('Ctrl Pts',(-0.283824062622952,2.78024166545816,
0.614777903021357));
#39317=CARTESIAN_POINT('Ctrl Pts',(-2.47829466728951,1.29193683314281,0.772113218692479));
#39318=CARTESIAN_POINT('Ctrl Pts',(-2.44182858239548,-1.35964121596809,
0.929448534363604));
#39319=CARTESIAN_POINT('Ctrl Pts',(-0.207121339063888,-2.78711087979173,
1.08678385003473));
#39320=CARTESIAN_POINT('Ctrl Pts',(2.21401803077907,-1.70561830406782,1.24411916570585));
#39321=CARTESIAN_POINT('Ctrl Pts',(2.64205485235054,0.911349150745493,1.40145448137697));
#39322=CARTESIAN_POINT('Ctrl Pts',(0.691640660298454,2.70787919402874,1.5587897970481));
#39323=CARTESIAN_POINT('Ctrl Pts',(-1.88140253096646,2.06671733364312,1.71612511271922));
#39324=CARTESIAN_POINT('Ctrl Pts',(-2.76076141176456,-0.43496057134077,
1.87346042839035));
#39325=CARTESIAN_POINT('Ctrl Pts',(-1.15481219883121,-2.54507342378116,
2.03079574406147));
#39326=CARTESIAN_POINT('Ctrl Pts',(1.49072764255621,-2.36404822464922,2.18813105973259));
#39327=CARTESIAN_POINT('Ctrl Pts',(2.79427705549031,-0.0548463935276453,
2.34546637540372));
#39328=CARTESIAN_POINT('Ctrl Pts',(1.5823475414007,2.30372918060613,2.50280169107483));
#39329=CARTESIAN_POINT('Ctrl Pts',(-1.05405113312049,2.58842974112365,2.66013700674597));
#39330=CARTESIAN_POINT('Ctrl Pts',(-2.74156638658485,0.542960359863138,
2.81747232241708));
#39331=CARTESIAN_POINT('Ctrl Pts',(-1.9610543025963,-1.99129560121778,2.97480763808821));
#39332=CARTESIAN_POINT('Ctrl Pts',(0.584848394656438,-2.73293698550247,
3.13214295375933));
#39333=CARTESIAN_POINT('Ctrl Pts',(2.60425579784155,-1.01431944186932,3.28947826943046));
#39334=CARTESIAN_POINT('Ctrl Pts',(2.27924634057658,1.61741407950708,3.44681358510158));
#39335=CARTESIAN_POINT('Ctrl Pts',(-0.0975982492034651,2.79311059143494,
3.6041489007727));
#39336=CARTESIAN_POINT('Ctrl Pts',(-2.38658243027454,1.45437838755459,3.76148421644382));
#39337=CARTESIAN_POINT('Ctrl Pts',(-2.52710481755741,-1.19362198012869,
3.91881953211495));
#39338=CARTESIAN_POINT('Ctrl Pts',(-0.392663608746353,-2.76709368867159,
4.07615484778607));
#39339=CARTESIAN_POINT('Ctrl Pts',(2.09526330020315,-1.8495577562663,4.23349016345719));
#39340=CARTESIAN_POINT('Ctrl Pts',(2.69698125586998,0.732996791565816,4.39082547912832));
#39341=CARTESIAN_POINT('Ctrl Pts',(0.870808554093777,2.65568911080063,4.54816079479944));
#39342=CARTESIAN_POINT('Ctrl Pts',(-1.73928800639316,2.18766300463189,4.70549611047057));
#39343=CARTESIAN_POINT('Ctrl Pts',(-2.78363356575401,-0.249752602863106,
4.86283142614169));
#39344=CARTESIAN_POINT('Ctrl Pts',(-1.32208186928512,-2.46233460804071,
5.02016674181281));
#39345=CARTESIAN_POINT('Ctrl Pts',(1.32964132424929,-2.45826079574207,5.17750205748394));
#39346=CARTESIAN_POINT('Ctrl Pts',(2.78438780839412,-0.241198514719961,
5.33483737315506));
#39347=CARTESIAN_POINT('Ctrl Pts',(1.73255804842731,2.19299676239354,5.49217268882618));
#39348=CARTESIAN_POINT('Ctrl Pts',(-0.878964234485193,2.65300095467984,
5.64950800449731));
#39349=CARTESIAN_POINT('Ctrl Pts',(-2.69922070918587,0.72470666765315,5.80684332016843));
#39350=CARTESIAN_POINT('Ctrl Pts',(-2.08957051396587,-1.85598686908106,
5.96417863583956));
#39351=CARTESIAN_POINT('Ctrl Pts',(0.401163844498212,-2.76587414046649,
6.12151395151068));
#39352=CARTESIAN_POINT('Ctrl Pts',(2.53076037597685,-1.18585163930103,6.2788492671818));
#39353=CARTESIAN_POINT('Ctrl Pts',(2.38210248511723,1.46170446446183,6.43618458285292));
#39354=CARTESIAN_POINT('Ctrl Pts',(0.0890157606711408,2.793397283841,6.59351989852405));
#39355=CARTESIAN_POINT('Ctrl Pts',(-2.28420520026003,1.61040330172691,6.75085521419516));
#39356=CARTESIAN_POINT('Ctrl Pts',(-2.60112693645964,-1.02231641451357,
6.9081905298663));
#39357=CARTESIAN_POINT('Ctrl Pts',(-0.57644849505612,-2.73472106868152,
7.06552584553741));
#39358=CARTESIAN_POINT('Ctrl Pts',(1.96716344393165,-1.98526073259378,7.22286116120855));
#39359=CARTESIAN_POINT('Ctrl Pts',(2.73988515609665,0.551381466653972,7.38019647687966));
#39360=CARTESIAN_POINT('Ctrl Pts',(1.04609303646807,2.5916561403346,7.53753179255079));
#39361=CARTESIAN_POINT('Ctrl Pts',(-1.58941846186445,2.2988564868904,7.69486710822191));
#39362=CARTESIAN_POINT('Ctrl Pts',(-2.79409530723714,-0.0634318507917163,
7.85220242389303));
#39363=CARTESIAN_POINT('Ctrl Pts',(-1.48345697628832,-2.36861723168749,
8.00953773956416));
#39364=CARTESIAN_POINT('Ctrl Pts',(1.16262680634646,-2.54151354917186,8.16687305523529));
#39365=CARTESIAN_POINT('Ctrl Pts',(2.76208455499713,-0.426475157784177,
8.3242083709064));
#39366=CARTESIAN_POINT('Ctrl Pts',(1.8750440359881,2.07248692819523,8.48154368657753));
#39367=CARTESIAN_POINT('Ctrl Pts',(-0.699958537943023,2.7057439570526,8.63887900224866));
#39368=CARTESIAN_POINT('Ctrl Pts',(-2.6448406647993,0.903221864868725,8.79621431791976));
#39369=CARTESIAN_POINT('Ctrl Pts',(-2.20877058145475,-1.7124032551425,8.95354963359091));
#39370=CARTESIAN_POINT('Ctrl Pts',(0.215690902196592,-2.78647992051942,
9.11088494926201));
#39371=CARTESIAN_POINT('Ctrl Pts',(2.4459813653409,-1.35209655994371,9.26822026493315));
#39372=CARTESIAN_POINT('Ctrl Pts',(2.47433880171217,1.29947749716991,9.42555558060427));
#39373=CARTESIAN_POINT('Ctrl Pts',(0.275231669725872,2.78123058171878,9.58289089627539));
#39374=CARTESIAN_POINT('Ctrl Pts',(-2.17164161907558,1.7592467736877,9.74022621194653));
#39375=CARTESIAN_POINT('Ctrl Pts',(-2.66355657074516,-0.846449946443288,
9.89756152761763));
#39376=CARTESIAN_POINT('Ctrl Pts',(-0.757654725048104,-2.69016151139635,
10.0548968432888));
#39377=CARTESIAN_POINT('Ctrl Pts',(1.83027666927001,-2.11210170665972,10.2122321589599));
#39378=CARTESIAN_POINT('Ctrl Pts',(2.77060484795253,0.367287133540841,10.369567474631));
#39379=CARTESIAN_POINT('Ctrl Pts',(1.21665350181368,2.51610800548609,10.5269027903021));
#39380=CARTESIAN_POINT('Ctrl Pts',(-1.43234772356642,2.39972494583597,10.6842381059733));
#39381=CARTESIAN_POINT('Ctrl Pts',(-2.79231938150401,0.123316482315984,
10.8415734216444));
#39382=CARTESIAN_POINT('Ctrl Pts',(-1.63779792657952,-2.26461658842463,
10.9989087373155));
#39383=CARTESIAN_POINT('Ctrl Pts',(0.989622905930635,-2.61290295808564,
11.1562440529866));
#39384=CARTESIAN_POINT('Ctrl Pts',(2.72902843688469,-0.61088887604173,11.3135793686578));
#39385=CARTESIAN_POINT('Ctrl Pts',(2.00599839187704,1.9449087769569,11.4709146843289));
#39386=CARTESIAN_POINT('Ctrl Pts',(0.328567026486064,2.47549058867235,11.5758048947763));
#39387=CARTESIAN_POINT('Ctrl Pts',(-0.439445221994061,2.3306835819919,11.62825));
#39388=CARTESIAN_POINT('Ctrl Pts',(-1.12236674703447,2.30288577939268,-0.219489327336923));
#39389=CARTESIAN_POINT('Ctrl Pts',(-1.881218999262,1.93304089110777,-0.167044222113215));
#39390=CARTESIAN_POINT('Ctrl Pts',(-2.9924775967461,0.391476088928602,-0.0621540116657994));
#39391=CARTESIAN_POINT('Ctrl Pts',(-1.97064588273166,-2.28935795203269,
0.0951813040053245));
#39392=CARTESIAN_POINT('Ctrl Pts',(0.82766540978493,-2.90224865758394,0.252516619676447));
#39393=CARTESIAN_POINT('Ctrl Pts',(2.87963202931947,-0.905958614903406,
0.409851935347572));
#39394=CARTESIAN_POINT('Ctrl Pts',(2.33993710190716,1.90770828264466,0.567187251018694));
#39395=CARTESIAN_POINT('Ctrl Pts',(-0.306571073860874,3.00306346507554,
0.724522566689817));
#39396=CARTESIAN_POINT('Ctrl Pts',(-2.67691699735827,1.39547879991837,0.881857882360941));
#39397=CARTESIAN_POINT('Ctrl Pts',(-2.63752834686069,-1.46860933422193,
1.03919319803207));
#39398=CARTESIAN_POINT('Ctrl Pts',(-0.223721028969555,-3.01048321093979,
1.19652851370319));
#39399=CARTESIAN_POINT('Ctrl Pts',(2.39145997337443,-1.84231467283839,1.35386382937431));
#39400=CARTESIAN_POINT('Ctrl Pts',(2.85380170306596,0.984389009248359,1.51119914504543));
#39401=CARTESIAN_POINT('Ctrl Pts',(0.747072034675363,2.92490152077689,1.66853446071656));
#39402=CARTESIAN_POINT('Ctrl Pts',(-2.03218708432488,2.23235389729304,1.82586977638768));
#39403=CARTESIAN_POINT('Ctrl Pts',(-2.98202197113476,-0.469820381720866,
1.98320509205881));
#39404=CARTESIAN_POINT('Ctrl Pts',(-1.24736434476896,-2.74904772122835,
2.14054040772993));
#39405=CARTESIAN_POINT('Ctrl Pts',(1.61020165094208,-2.55351430104939,2.29787572340105));
#39406=CARTESIAN_POINT('Ctrl Pts',(3.01822371806624,-0.0592420445461263,
2.45521103907218));
#39407=CARTESIAN_POINT('Ctrl Pts',(1.70916440454448,2.48836100172844,2.6125463547433));
#39408=CARTESIAN_POINT('Ctrl Pts',(-1.13852780768032,2.79587882019688,2.76988167041443));
#39409=CARTESIAN_POINT('Ctrl Pts',(-2.9612885652785,0.586475787319947,2.92721698608554));
#39410=CARTESIAN_POINT('Ctrl Pts',(-2.11822252803541,-2.15088750826171,
3.08455230175667));
#39411=CARTESIAN_POINT('Ctrl Pts',(0.631720928587459,-2.95196756292179,
3.24188761742779));
#39412=CARTESIAN_POINT('Ctrl Pts',(2.81297325242419,-1.09561182958951,3.39922293309892));
#39413=CARTESIAN_POINT('Ctrl Pts',(2.46191599037299,1.74704134191371,3.55655824877004));
#39414=CARTESIAN_POINT('Ctrl Pts',(-0.105420237413036,3.01696376802969,
3.71389356444116));
#39415=CARTESIAN_POINT('Ctrl Pts',(-2.57785450516496,1.57093919364055,3.87122888011228));
#39416=CARTESIAN_POINT('Ctrl Pts',(-2.72963902538035,-1.28928452665457,
4.02856419578341));
#39417=CARTESIAN_POINT('Ctrl Pts',(-0.424133539231963,-2.98886174685155,
4.18589951145453));
#39418=CARTESIAN_POINT('Ctrl Pts',(2.26318767347756,-1.99779011781522,4.34323482712566));
#39419=CARTESIAN_POINT('Ctrl Pts',(2.91313016998542,0.791742643136777,4.50057014279678));
#39420=CARTESIAN_POINT('Ctrl Pts',(0.940599296228219,2.86852867588043,4.6579054584679));
#39421=CARTESIAN_POINT('Ctrl Pts',(-1.87868282535885,2.36299272999521,4.81524077413902));
#39422=CARTESIAN_POINT('Ctrl Pts',(-3.00672720840483,-0.269768965152914,
4.97257608981016));
#39423=CARTESIAN_POINT('Ctrl Pts',(-1.42803980273229,-2.65967782299944,
5.12991140548127));
#39424=CARTESIAN_POINT('Ctrl Pts',(1.43620510839645,-2.65527751599392,5.28724672115241));
#39425=CARTESIAN_POINT('Ctrl Pts',(3.00754189963992,-0.260529311672868,
5.44458203682351));
#39426=CARTESIAN_POINT('Ctrl Pts',(1.87141349653044,2.36875396048986,5.60191735249465));
#39427=CARTESIAN_POINT('Ctrl Pts',(-0.949408611663097,2.86562507813386,
5.75925266816576));
#39428=CARTESIAN_POINT('Ctrl Pts',(-2.9155491037487,0.782788109236974,5.9165879838369));
#39429=CARTESIAN_POINT('Ctrl Pts',(-2.25703864025646,-2.00473449033026,
6.07392329950801));
#39430=CARTESIAN_POINT('Ctrl Pts',(0.433315024333776,-2.98754445824887,
6.23125861517914));
#39431=CARTESIAN_POINT('Ctrl Pts',(2.73358755765012,-1.28089143373012,6.38859393085026));
#39432=CARTESIAN_POINT('Ctrl Pts',(2.57301551588047,1.57885241721953,6.54592924652138));
#39433=CARTESIAN_POINT('Ctrl Pts',(0.0961499074014511,3.01727343732968,
6.70326456219251));
#39434=CARTESIAN_POINT('Ctrl Pts',(-2.46727227667312,1.73946868703451,6.86059987786364));
#39435=CARTESIAN_POINT('Ctrl Pts',(-2.80959362919934,-1.104249717683,7.01793519353475));
#39436=CARTESIAN_POINT('Ctrl Pts',(-0.622647821053927,-2.95389463101813,
7.17527050920589));
#39437=CARTESIAN_POINT('Ctrl Pts',(2.12482128503379,-2.14436897654329,7.33260582487699));
#39438=CARTESIAN_POINT('Ctrl Pts',(2.95947259297716,0.59557180168919,7.48994114054813));
#39439=CARTESIAN_POINT('Ctrl Pts',(1.12993191128569,2.79936379839662,7.64727645621924));
#39440=CARTESIAN_POINT('Ctrl Pts',(-1.71680202222819,2.4830977871468,7.80461177189038));
#39441=CARTESIAN_POINT('Ctrl Pts',(-3.01802740364303,-0.0685155812177535,
7.96194708756148));
#39442=CARTESIAN_POINT('Ctrl Pts',(-1.60234827887482,-2.55844949005786,
8.11928240323263));
#39443=CARTESIAN_POINT('Ctrl Pts',(1.25580525212405,-2.74520254132467,8.27661771890373));
#39444=CARTESIAN_POINT('Ctrl Pts',(2.98345115736347,-0.460654906735591,
8.43395303457487));
#39445=CARTESIAN_POINT('Ctrl Pts',(2.02531898929576,2.23858589461288,8.591288350246));
#39446=CARTESIAN_POINT('Ctrl Pts',(-0.756056546623237,2.92259515574686,
8.74862366591711));
#39447=CARTESIAN_POINT('Ctrl Pts',(-2.85681078378342,0.975610363999675,
8.90595898158824));
#39448=CARTESIAN_POINT('Ctrl Pts',(-2.38579196848608,-1.84964340218511,
9.06329429725935));
#39449=CARTESIAN_POINT('Ctrl Pts',(0.232977397678477,-3.00980168358836,
9.2206296129305));
#39450=CARTESIAN_POINT('Ctrl Pts',(2.6420139535965,-1.46046001355504,9.37796492860159));
#39451=CARTESIAN_POINT('Ctrl Pts',(2.67264408988566,1.40362380865033,9.53530024427275));
#39452=CARTESIAN_POINT('Ctrl Pts',(0.297290045701602,3.00413163779202,9.69263555994384));
#39453=CARTESIAN_POINT('Ctrl Pts',(-2.34568731434669,1.90024118325806,9.84997087561499));
#39454=CARTESIAN_POINT('Ctrl Pts',(-2.87702667151006,-0.914288473825907,
10.0073061912861));
#39455=CARTESIAN_POINT('Ctrl Pts',(-0.818376780767691,-2.90576385873112,
10.1646415069572));
#39456=CARTESIAN_POINT('Ctrl Pts',(1.97696375273877,-2.2813755899699,10.3219768226283));
#39457=CARTESIAN_POINT('Ctrl Pts',(2.99265430714862,0.396723272524227,10.4793121382995));
#39458=CARTESIAN_POINT('Ctrl Pts',(1.31416190410585,2.71776087645035,10.6366474539706));
#39459=CARTESIAN_POINT('Ctrl Pts',(-1.54714288738549,2.59205032447523,10.7939827696417));
#39460=CARTESIAN_POINT('Ctrl Pts',(-3.01610914676913,0.133199652133039,
10.9513180853128));
#39461=CARTESIAN_POINT('Ctrl Pts',(-1.76905884750739,-2.44611374025332,
11.108653400984));
#39462=CARTESIAN_POINT('Ctrl Pts',(1.06893599571762,-2.82231343724637,11.2659887166551));
#39463=CARTESIAN_POINT('Ctrl Pts',(2.94774576461505,-0.659848418090555,
11.4233240323262));
#39464=CARTESIAN_POINT('Ctrl Pts',(2.1667686505423,2.10078302312668,11.5806593479973));
#39465=CARTESIAN_POINT('Ctrl Pts',(0.35489995180194,2.67388818653474,11.6855495584447));
#39466=CARTESIAN_POINT('Ctrl Pts',(-0.474664453622185,2.51747565713064,
11.7379946636685));
#39467=CARTESIAN_POINT('Ctrl Pts',(-1.20564430054384,2.47375567929493,-0.109744663668461));
#39468=CARTESIAN_POINT('Ctrl Pts',(-2.02080199767838,2.07646897882546,-0.0572995584447534));
#39469=CARTESIAN_POINT('Ctrl Pts',(-3.21451394435451,0.420522896515832,
0.0475906520026618));
#39470=CARTESIAN_POINT('Ctrl Pts',(-2.11686419183683,-2.45922411196328,
0.204925967673786));
#39471=CARTESIAN_POINT('Ctrl Pts',(0.88907666473643,-3.11759018344267,0.362261283344908));
#39472=CARTESIAN_POINT('Ctrl Pts',(3.09329544285396,-0.973179082036162,
0.519596599016033));
#39473=CARTESIAN_POINT('Ctrl Pts',(2.51355614196476,2.04925673729017,0.676931914687155));
#39474=CARTESIAN_POINT('Ctrl Pts',(-0.329318085098797,3.22588526469291,
0.83426723035828));
#39475=CARTESIAN_POINT('Ctrl Pts',(-2.87553932742704,1.49902076669393,0.991602546029402));
#39476=CARTESIAN_POINT('Ctrl Pts',(-2.8332281113259,-1.57757745247578,1.14893786170053));
#39477=CARTESIAN_POINT('Ctrl Pts',(-0.240320718875223,-3.23385554208785,
1.30627317737165));
#39478=CARTESIAN_POINT('Ctrl Pts',(2.5689019159698,-1.97901104160895,1.46360849304277));
#39479=CARTESIAN_POINT('Ctrl Pts',(3.06554855378139,1.05742886775122,1.6209438087139));
#39480=CARTESIAN_POINT('Ctrl Pts',(0.802503409052275,3.14192384752506,1.77827912438502));
#39481=CARTESIAN_POINT('Ctrl Pts',(-2.18297163768331,2.39799046094296,1.93561444005614));
#39482=CARTESIAN_POINT('Ctrl Pts',(-3.20328253050495,-0.504680192100957,
2.09294975572727));
#39483=CARTESIAN_POINT('Ctrl Pts',(-1.33991649070671,-2.95302201867555,
2.25028507139839));
#39484=CARTESIAN_POINT('Ctrl Pts',(1.72967565932795,-2.74298037744955,2.40762038706951));
#39485=CARTESIAN_POINT('Ctrl Pts',(3.24217038064216,-0.0636376955646108,
2.56495570274064));
#39486=CARTESIAN_POINT('Ctrl Pts',(1.83598126768827,2.67299282285076,2.72229101841176));
#39487=CARTESIAN_POINT('Ctrl Pts',(-1.22300448224015,3.00332789927011,2.87962633408289));
#39488=CARTESIAN_POINT('Ctrl Pts',(-3.18101074397215,0.629991214776759,
3.036961649754));
#39489=CARTESIAN_POINT('Ctrl Pts',(-2.27539075347452,-2.31047941530565,
3.19429696542514));
#39490=CARTESIAN_POINT('Ctrl Pts',(0.678593462518484,-3.1709981403411,3.35163228109625));
#39491=CARTESIAN_POINT('Ctrl Pts',(3.02169070700682,-1.1769042173097,3.50896759676738));
#39492=CARTESIAN_POINT('Ctrl Pts',(2.64458564016939,1.87666860432035,3.6663029124385));
#39493=CARTESIAN_POINT('Ctrl Pts',(-0.113242225622608,3.24081694462443,
3.82363822810962));
#39494=CARTESIAN_POINT('Ctrl Pts',(-2.76912658005537,1.68749999972651,3.98097354378075));
#39495=CARTESIAN_POINT('Ctrl Pts',(-2.93217323320329,-1.38494707318046,
4.13830885945187));
#39496=CARTESIAN_POINT('Ctrl Pts',(-0.45560346971757,-3.21062980503151,
4.295644175123));
#39497=CARTESIAN_POINT('Ctrl Pts',(2.43111204675198,-2.14602247936414,4.45297949079412));
#39498=CARTESIAN_POINT('Ctrl Pts',(3.12927908410086,0.850488494707743,4.61031480646524));
#39499=CARTESIAN_POINT('Ctrl Pts',(1.01039003836266,3.08136824096022,4.76765012213636));
#39500=CARTESIAN_POINT('Ctrl Pts',(-2.01807764432454,2.53832245535854,4.92498543780749));
#39501=CARTESIAN_POINT('Ctrl Pts',(-3.22982085105565,-0.289785327442726,
5.08232075347861));
#39502=CARTESIAN_POINT('Ctrl Pts',(-1.53399773617946,-2.85702103795818,
5.23965606914974));
#39503=CARTESIAN_POINT('Ctrl Pts',(1.5427688925436,-2.85229423624577,5.39699138482085));
#39504=CARTESIAN_POINT('Ctrl Pts',(3.23069599088573,-0.279860108625777,
5.55432670049199));
#39505=CARTESIAN_POINT('Ctrl Pts',(2.01026894463356,2.54451115858618,5.7116620161631));
#39506=CARTESIAN_POINT('Ctrl Pts',(-1.019852988841,3.07824920158788,5.86899733183423));
#39507=CARTESIAN_POINT('Ctrl Pts',(-3.13187749831153,0.840869550820803,
6.02633264750535));
#39508=CARTESIAN_POINT('Ctrl Pts',(-2.42450676654705,-2.15348211157947,
6.18366796317648));
#39509=CARTESIAN_POINT('Ctrl Pts',(0.465466204169338,-3.20921477603124,
6.3410032788476));
#39510=CARTESIAN_POINT('Ctrl Pts',(2.93641473932339,-1.3759312281592,6.49833859451872));
#39511=CARTESIAN_POINT('Ctrl Pts',(2.76392854664371,1.69600036997724,6.65567391018985));
#39512=CARTESIAN_POINT('Ctrl Pts',(0.103284054131762,3.24114959081836,6.81300922586097));
#39513=CARTESIAN_POINT('Ctrl Pts',(-2.65033935308621,1.86853407234211,6.97034454153209));
#39514=CARTESIAN_POINT('Ctrl Pts',(-3.01806032193904,-1.18618302085242,
7.12767985720322));
#39515=CARTESIAN_POINT('Ctrl Pts',(-0.668847147051728,-3.17306819335475,
7.28501517287434));
#39516=CARTESIAN_POINT('Ctrl Pts',(2.28247912613591,-2.30347722049279,7.44235048854546));
#39517=CARTESIAN_POINT('Ctrl Pts',(3.17906002985769,0.639762136724403,7.59968580421659));
#39518=CARTESIAN_POINT('Ctrl Pts',(1.2137707861033,3.00707145645863,7.75702111988771));
#39519=CARTESIAN_POINT('Ctrl Pts',(-1.84418558259193,2.66733908740319,7.91435643555884));
#39520=CARTESIAN_POINT('Ctrl Pts',(-3.24195950004891,-0.0735993116437874,
8.07169175122995));
#39521=CARTESIAN_POINT('Ctrl Pts',(-1.7212395814613,-2.74828174842822,8.22902706690109));
#39522=CARTESIAN_POINT('Ctrl Pts',(1.34898369790163,-2.94889153347749,8.38636238257219));
#39523=CARTESIAN_POINT('Ctrl Pts',(3.20481775972981,-0.494834655687006,
8.54369769824334));
#39524=CARTESIAN_POINT('Ctrl Pts',(2.17559394260342,2.40468486103055,8.70103301391445));
#39525=CARTESIAN_POINT('Ctrl Pts',(-0.812154555303452,3.13944635444111,
8.85836832958556));
#39526=CARTESIAN_POINT('Ctrl Pts',(-3.06878090276754,1.04799886313063,9.01570364525671));
#39527=CARTESIAN_POINT('Ctrl Pts',(-2.56281335551741,-1.98688354922771,
9.17303896092782));
#39528=CARTESIAN_POINT('Ctrl Pts',(0.250263893160364,-3.23312344665729,
9.33037427659894));
#39529=CARTESIAN_POINT('Ctrl Pts',(2.83804654185209,-1.56882346716636,9.48770959227006));
#39530=CARTESIAN_POINT('Ctrl Pts',(2.87094937805915,1.50777012013074,9.64504490794121));
#39531=CARTESIAN_POINT('Ctrl Pts',(0.31934842167733,3.22703269386527,9.8023802236123));
#39532=CARTESIAN_POINT('Ctrl Pts',(-2.5197330096178,2.04123559282842,9.95971553928346));
#39533=CARTESIAN_POINT('Ctrl Pts',(-3.09049677227496,-0.982127001208522,
10.1170508549545));
#39534=CARTESIAN_POINT('Ctrl Pts',(-0.879098836487281,-3.1213662060659,
10.2743861706257));
#39535=CARTESIAN_POINT('Ctrl Pts',(2.12365083620754,-2.45064947328008,10.4317214862968));
#39536=CARTESIAN_POINT('Ctrl Pts',(3.2147037663447,0.426159411507612,10.5890568019679));
#39537=CARTESIAN_POINT('Ctrl Pts',(1.41167030639802,2.9194137474146,10.7463921176391));
#39538=CARTESIAN_POINT('Ctrl Pts',(-1.66193805120456,2.78437570311449,10.9037274333102));
#39539=CARTESIAN_POINT('Ctrl Pts',(-3.23989891203425,0.143082821950096,
11.0610627489813));
#39540=CARTESIAN_POINT('Ctrl Pts',(-1.90031976843527,-2.627610892082,11.2183980646524));
#39541=CARTESIAN_POINT('Ctrl Pts',(1.1482490855046,-3.0317239164071,11.3757333803236));
#39542=CARTESIAN_POINT('Ctrl Pts',(3.16646309234541,-0.708807960139384,
11.5330686959947));
#39543=CARTESIAN_POINT('Ctrl Pts',(2.32753890920755,2.25665726929647,11.6904040116658));
#39544=CARTESIAN_POINT('Ctrl Pts',(0.381232877117816,2.87228578439713,11.7952942221132));
#39545=CARTESIAN_POINT('Ctrl Pts',(-0.50988368525031,2.70426773226937,11.8477393273369));
#39546=CARTESIAN_POINT('Ctrl Pts',(-1.28892185405322,2.64462557919718,0.));
#39547=CARTESIAN_POINT('Ctrl Pts',(-2.16038499609476,2.21989706654315,0.0524451052237078));
#39548=CARTESIAN_POINT('Ctrl Pts',(-3.43655029196293,0.449569704103062,
0.157335315671123));
#39549=CARTESIAN_POINT('Ctrl Pts',(-2.26308250094201,-2.62909027189387,
0.314670631342247));
#39550=CARTESIAN_POINT('Ctrl Pts',(0.950487919687924,-3.33293170930141,
0.47200594701337));
#39551=CARTESIAN_POINT('Ctrl Pts',(3.30695885638846,-1.04039954916892,0.629341262684495));
#39552=CARTESIAN_POINT('Ctrl Pts',(2.68717518202235,2.19080519193567,0.786676578355616));
#39553=CARTESIAN_POINT('Ctrl Pts',(-0.352065096336719,3.44870706431028,
0.944011894026741));
#39554=CARTESIAN_POINT('Ctrl Pts',(-3.0741616574958,1.60256273346949,1.10134720969786));
#39555=CARTESIAN_POINT('Ctrl Pts',(-3.02892787579111,-1.68654557072963,
1.25868252536899));
#39556=CARTESIAN_POINT('Ctrl Pts',(-0.256920408780888,-3.45722787323591,
1.41601784104011));
#39557=CARTESIAN_POINT('Ctrl Pts',(2.74634385856517,-2.11570741037952,1.57335315671124));
#39558=CARTESIAN_POINT('Ctrl Pts',(3.27729540449682,1.13046872625408,1.73068847238236));
#39559=CARTESIAN_POINT('Ctrl Pts',(0.857934783429182,3.35894617427322,1.88802378805348));
#39560=CARTESIAN_POINT('Ctrl Pts',(-2.33375619104173,2.56362702459287,2.0453591037246));
#39561=CARTESIAN_POINT('Ctrl Pts',(-3.42454308987515,-0.539540002481048,
2.20269441939573));
#39562=CARTESIAN_POINT('Ctrl Pts',(-1.43246863664446,-3.15699631612275,
2.36002973506685));
#39563=CARTESIAN_POINT('Ctrl Pts',(1.84914966771382,-2.93244645384971,2.51736505073797));
#39564=CARTESIAN_POINT('Ctrl Pts',(3.46611704321809,-0.0680333465830936,
2.6747003664091));
#39565=CARTESIAN_POINT('Ctrl Pts',(1.96279813083206,2.85762464397308,2.83203568208022));
#39566=CARTESIAN_POINT('Ctrl Pts',(-1.30748115679998,3.21077697834334,2.98937099775135));
#39567=CARTESIAN_POINT('Ctrl Pts',(-3.40073292266579,0.673506642233569,
3.14670631342246));
#39568=CARTESIAN_POINT('Ctrl Pts',(-2.43255897891363,-2.47007132234958,
3.3040416290936));
#39569=CARTESIAN_POINT('Ctrl Pts',(0.725465996449509,-3.39002871776042,
3.46137694476471));
#39570=CARTESIAN_POINT('Ctrl Pts',(3.23040816158946,-1.2581966050299,3.61871226043584));
#39571=CARTESIAN_POINT('Ctrl Pts',(2.8272552899658,2.00629586672699,3.77604757610696));
#39572=CARTESIAN_POINT('Ctrl Pts',(-0.12106421383218,3.46467012121918,3.93338289177809));
#39573=CARTESIAN_POINT('Ctrl Pts',(-2.96039865494578,1.80406080581246,4.09071820744921));
#39574=CARTESIAN_POINT('Ctrl Pts',(-3.13470744102623,-1.48060961970634,
4.24805352312033));
#39575=CARTESIAN_POINT('Ctrl Pts',(-0.48707340020318,-3.43239786321147,
4.40538883879146));
#39576=CARTESIAN_POINT('Ctrl Pts',(2.59903642002639,-2.29425484091306,4.56272415446258));
#39577=CARTESIAN_POINT('Ctrl Pts',(3.3454279982163,0.909234346278705,4.7200594701337));
#39578=CARTESIAN_POINT('Ctrl Pts',(1.0801807804971,3.29420780604002,4.87739478580482));
#39579=CARTESIAN_POINT('Ctrl Pts',(-2.15747246329023,2.71365218072187,5.03473010147595));
#39580=CARTESIAN_POINT('Ctrl Pts',(-3.45291449370647,-0.309801689732533,
5.19206541714708));
#39581=CARTESIAN_POINT('Ctrl Pts',(-1.63995566962662,-3.05436425291692,
5.34940073281819));
#39582=CARTESIAN_POINT('Ctrl Pts',(1.64933267669075,-3.04931095649762,5.50673604848933));
#39583=CARTESIAN_POINT('Ctrl Pts',(3.45385008213154,-0.299190905578683,
5.66407136416044));
#39584=CARTESIAN_POINT('Ctrl Pts',(2.14912439273668,2.7202683566825,5.82140667983157));
#39585=CARTESIAN_POINT('Ctrl Pts',(-1.0902973660189,3.2908733250419,5.97874199550268));
#39586=CARTESIAN_POINT('Ctrl Pts',(-3.34820589287437,0.898950992404627,
6.13607731117382));
#39587=CARTESIAN_POINT('Ctrl Pts',(-2.59197489283764,-2.30222973282867,
6.29341262684493));
#39588=CARTESIAN_POINT('Ctrl Pts',(0.497617384004899,-3.43088509381362,
6.45074794251607));
#39589=CARTESIAN_POINT('Ctrl Pts',(3.13924192099666,-1.47097102258828,6.60808325818718));
#39590=CARTESIAN_POINT('Ctrl Pts',(2.95484157740695,1.81314832273494,6.76541857385831));
#39591=CARTESIAN_POINT('Ctrl Pts',(0.110418200862072,3.46502574430704,6.92275388952943));
#39592=CARTESIAN_POINT('Ctrl Pts',(-2.8334064294993,1.9975994576497,7.08008920520056));
#39593=CARTESIAN_POINT('Ctrl Pts',(-3.22652701467874,-1.26811632402185,
7.23742452087168));
#39594=CARTESIAN_POINT('Ctrl Pts',(-0.715046473049532,-3.39224175569136,
7.3947598365428));
#39595=CARTESIAN_POINT('Ctrl Pts',(2.44013696723805,-2.46258546444229,7.55209515221393));
#39596=CARTESIAN_POINT('Ctrl Pts',(3.39864746673821,0.683952471759619,7.70943046788505));
#39597=CARTESIAN_POINT('Ctrl Pts',(1.29760966092091,3.21477911452065,7.86676578355617));
#39598=CARTESIAN_POINT('Ctrl Pts',(-1.97156914295567,2.85158038765959,8.0241010992273));
#39599=CARTESIAN_POINT('Ctrl Pts',(-3.4658915964548,-0.0786830420698247,
8.18143641489842));
#39600=CARTESIAN_POINT('Ctrl Pts',(-1.84013088404779,-2.93811400679859,
8.33877173056954));
#39601=CARTESIAN_POINT('Ctrl Pts',(1.44216214367922,-3.1525805256303,8.49610704624066));
#39602=CARTESIAN_POINT('Ctrl Pts',(3.42618436209615,-0.529014404638419,
8.6534423619118));
#39603=CARTESIAN_POINT('Ctrl Pts',(2.32586889591107,2.57078382744821,8.81077767758291));
#39604=CARTESIAN_POINT('Ctrl Pts',(-0.868252563983666,3.35629755313536,
8.96811299325404));
#39605=CARTESIAN_POINT('Ctrl Pts',(-3.28075102175166,1.12038736226158,9.12544830892515));
#39606=CARTESIAN_POINT('Ctrl Pts',(-2.73983474254873,-2.12412369627032,
9.28278362459629));
#39607=CARTESIAN_POINT('Ctrl Pts',(0.267550388642249,-3.45644520972622,
9.44011894026741));
#39608=CARTESIAN_POINT('Ctrl Pts',(3.03407913010768,-1.67718692077769,9.59745425593853));
#39609=CARTESIAN_POINT('Ctrl Pts',(3.06925466623264,1.61191643161116,9.75478957160966));
#39610=CARTESIAN_POINT('Ctrl Pts',(0.341406797653059,3.4499337499385,9.91212488728077));
#39611=CARTESIAN_POINT('Ctrl Pts',(-2.69377870488891,2.18223000239878,10.0694602029519));
#39612=CARTESIAN_POINT('Ctrl Pts',(-3.30396687303986,-1.04996552859114,
10.226795518623));
#39613=CARTESIAN_POINT('Ctrl Pts',(-0.939820892206868,-3.33696855340067,
10.3841308342941));
#39614=CARTESIAN_POINT('Ctrl Pts',(2.2703379196763,-2.61992335659027,10.5414661499653));
#39615=CARTESIAN_POINT('Ctrl Pts',(3.43675322554079,0.455595550491001,10.6988014656364));
#39616=CARTESIAN_POINT('Ctrl Pts',(1.50917870869019,3.12106661837885,10.8561367813075));
#39617=CARTESIAN_POINT('Ctrl Pts',(-1.77673321502363,2.97670108175376,11.0134720969786));
#39618=CARTESIAN_POINT('Ctrl Pts',(-3.46368867729937,0.152965991767152,
11.1708074126498));
#39619=CARTESIAN_POINT('Ctrl Pts',(-2.03158068936315,-2.80910804391069,
11.3281427283209));
#39620=CARTESIAN_POINT('Ctrl Pts',(1.22756217529158,-3.24113439556783,11.485478043992));
#39621=CARTESIAN_POINT('Ctrl Pts',(3.38518042007578,-0.757767502188211,
11.6428133596631));
#39622=CARTESIAN_POINT('Ctrl Pts',(2.48830916787281,2.41253151546626,11.8001486753343));
#39623=CARTESIAN_POINT('Ctrl Pts',(0.407565802433691,3.07068338225952,11.9050388857817));
#39624=CARTESIAN_POINT('Ctrl Pts',(-0.545102916878434,2.89105980740811,
11.9574839910054));
#39625=CARTESIAN_POINT('Ctrl Pts',(-2.93989309841074,-0.00232834448912937,
10.1778238829104));
#39626=CARTESIAN_POINT('Ctrl Pts',(-2.94219554736775,-0.304542880453153,
10.1941477614813));
#39627=CARTESIAN_POINT('Ctrl Pts',(-2.89923296915434,-0.606119063222061,
10.2104716400522));
#39628=CARTESIAN_POINT('Ctrl Pts',(-2.80824451487588,-0.892433444227729,
10.226795518623));
#39629=CARTESIAN_POINT('Ctrl Pts',(-2.5159182127622,-1.81229987019432,10.2792406238467));
#39630=CARTESIAN_POINT('Ctrl Pts',(-1.72786955248453,-2.5746342117975,10.3316857290704));
#39631=CARTESIAN_POINT('Ctrl Pts',(-0.798818753698492,-2.83629384979735,
10.3841308342941));
#39632=CARTESIAN_POINT('Ctrl Pts',(0.130232045087536,-3.0979534877972,10.4365759395179));
#39633=CARTESIAN_POINT('Ctrl Pts',(1.20028498238192,-2.85893842219374,10.4890210447416));
#39634=CARTESIAN_POINT('Ctrl Pts',(1.92971400200653,-2.22684440487846,10.5414661499653));
#39635=CARTESIAN_POINT('Ctrl Pts',(2.65914302163113,-1.59475038756318,10.593911255189));
#39636=CARTESIAN_POINT('Ctrl Pts',(3.04794812358597,-0.569577418536059,
10.6463563604127));
#39637=CARTESIAN_POINT('Ctrl Pts',(2.92108825508827,0.387254243958792,10.6988014656364));
#39638=CARTESIAN_POINT('Ctrl Pts',(2.79422838659058,1.34408590645364,10.7512465708601));
#39639=CARTESIAN_POINT('Ctrl Pts',(2.15170354764038,2.23257626241624,10.8036916760838));
#39640=CARTESIAN_POINT('Ctrl Pts',(1.28278914087964,2.6527605176267,10.8561367813075));
#39641=CARTESIAN_POINT('Ctrl Pts',(0.413874734118906,3.07294477283715,10.9085818865312));
#39642=CARTESIAN_POINT('Ctrl Pts',(-0.681429240452357,3.02482292729546,
10.9610269917549));
#39643=CARTESIAN_POINT('Ctrl Pts',(-1.51024047145062,2.53013948952684,11.0134720969786));
#39644=CARTESIAN_POINT('Ctrl Pts',(-1.74480463118476,2.39013776105746,11.0283147313191));
#39645=CARTESIAN_POINT('Ctrl Pts',(-1.95802372783935,2.21436813426865,11.0431573656595));
#39646=CARTESIAN_POINT('Ctrl Pts',(-2.14415473270596,2.01243073062332,11.058));
#39647=CARTESIAN_POINT('Ctrl Pts',(-1.37989654081095,-1.933266887693,1.56125112837913E-17));
#39648=CARTESIAN_POINT('Ctrl Pts',(-1.44414345926609,-1.89839188587405,
5.80920822621902E-18));
#39649=CARTESIAN_POINT('Ctrl Pts',(-1.5065284577229,-1.86047032724736,-1.41833741640826E-16));
#39650=CARTESIAN_POINT('Ctrl Pts',(-1.56680444439783,-1.81955553349441,
-1.49186218934005E-16));
#39651=CARTESIAN_POINT('Ctrl Pts',(-1.63448180748404,-1.77361675247786,
-1.62745475426733E-16));
#39652=CARTESIAN_POINT('Ctrl Pts',(-1.69950176926845,-1.72390575990714,
4.47554715783556E-16));
#39653=CARTESIAN_POINT('Ctrl Pts',(-1.76178079551988,-1.6707784873017,5.27355936696949E-16));
#39654=CARTESIAN_POINT('Ctrl Pts',(-1.80277525259689,-1.63580806744237,
5.79884178102324E-16));
#39655=CARTESIAN_POINT('Ctrl Pts',(-1.84258178887229,-1.59935636303953,
9.13682232518509E-17));
#39656=CARTESIAN_POINT('Ctrl Pts',(-1.88117141744704,-1.56151405921777,
1.59594559789866E-16));
#39657=CARTESIAN_POINT('Ctrl Pts',(-1.89157558896771,-1.55131137434519,
1.77989100856589E-16));
#39658=CARTESIAN_POINT('Ctrl Pts',(-1.90188938652621,-1.54100934347453,
3.40635361961997E-16));
#39659=CARTESIAN_POINT('Ctrl Pts',(-1.91210630257196,-1.53061605927472,
3.05311331771918E-16));
#39660=CARTESIAN_POINT('Ctrl Pts',(-1.9724409846318,-1.46923985779222,9.67098202152561E-17));
#39661=CARTESIAN_POINT('Ctrl Pts',(-2.02946085491381,-1.40462521591101,
1.4935214824922E-16));
#39662=CARTESIAN_POINT('Ctrl Pts',(-2.08307562783518,-1.33717477526203,
1.38777878078145E-16));
#39663=CARTESIAN_POINT('Ctrl Pts',(-2.12998855414138,-1.27815563969417,
1.29525391678454E-16));
#39664=CARTESIAN_POINT('Ctrl Pts',(-2.17429437900105,-1.21696417926775,
2.01441503266146E-16));
#39665=CARTESIAN_POINT('Ctrl Pts',(-2.21591583956505,-1.15384057343859,
1.52655665885959E-16));
#39666=CARTESIAN_POINT('Ctrl Pts',(-2.23664963326987,-1.12239545345888,
1.28352927004359E-16));
#39667=CARTESIAN_POINT('Ctrl Pts',(-2.25671701785544,-1.09047047206691,
-2.37280165770185E-16));
#39668=CARTESIAN_POINT('Ctrl Pts',(-2.2761066605572,-1.05809323638609,-2.63677968348475E-16));
#39669=CARTESIAN_POINT('Ctrl Pts',(-2.28578146762193,-1.0419380388242,-2.76849621421526E-16));
#39670=CARTESIAN_POINT('Ctrl Pts',(-2.29528887628369,-1.02566760843717,
-1.10809144900277E-17));
#39671=CARTESIAN_POINT('Ctrl Pts',(-2.30461525834334,-1.0093071858719,0.));
#39672=CARTESIAN_POINT('Ctrl Pts',(-2.34846766322256,-0.932380906234359,
5.21021705459412E-17));
#39673=CARTESIAN_POINT('Ctrl Pts',(-2.38837887518559,-0.853373340579809,
-1.59588577561705E-17));
#39674=CARTESIAN_POINT('Ctrl Pts',(-2.42425706703596,-0.772682188207588,
-2.77555756156289E-17));
#39675=CARTESIAN_POINT('Ctrl Pts',(-2.46075963346513,-0.690586798283878,
-3.97575872863117E-17));
#39676=CARTESIAN_POINT('Ctrl Pts',(-2.49308822244858,-0.606748001409621,
2.24945356107799E-18));
#39677=CARTESIAN_POINT('Ctrl Pts',(-2.52111243497218,-0.521542915861604,
-2.77555756156289E-17));
#39678=CARTESIAN_POINT('Ctrl Pts',(-2.54406484395513,-0.4517581906252,-5.23303143573299E-17));
#39679=CARTESIAN_POINT('Ctrl Pts',(-2.56412941494483,-0.381055975787894,
-5.2234519399031E-17));
#39680=CARTESIAN_POINT('Ctrl Pts',(-2.58121358727312,-0.309628512371508,
-5.55111512312578E-17));
#39681=CARTESIAN_POINT('Ctrl Pts',(-2.59402671651933,-0.256057914809218,
-5.79686251054279E-17));
#39682=CARTESIAN_POINT('Ctrl Pts',(-2.6051630020304,-0.202079063721199,
-1.68485553630616E-16));
#39683=CARTESIAN_POINT('Ctrl Pts',(-2.61457527537642,-0.147769877191515,
-1.94289029309402E-16));
#39684=CARTESIAN_POINT('Ctrl Pts',(-2.617136534184,-0.132991313371873,-2.01310646395843E-16));
#39685=CARTESIAN_POINT('Ctrl Pts',(-2.6195700893165,-0.118188277474481,
-3.31395093795537E-16));
#39686=CARTESIAN_POINT('Ctrl Pts',(-2.6218748923051,-0.103362317982878,
-3.33066907387547E-16));
#39687=CARTESIAN_POINT('Ctrl Pts',(-2.62397146608191,-0.089875821288789,
-3.34587679685255E-16));
#39688=CARTESIAN_POINT('Ctrl Pts',(-2.62596008221826,-0.076379405564125,
-2.78772373994456E-16));
#39689=CARTESIAN_POINT('Ctrl Pts',(-2.62784009463941,-0.0628763941457686,
-2.77555756156289E-16));
#39690=CARTESIAN_POINT('Ctrl Pts',(-2.64060982150785,0.0288409614284714,
-2.69292046128659E-16));
#39691=CARTESIAN_POINT('Ctrl Pts',(-2.64837710873961,0.12089024959815,-1.76997536955934E-16));
#39692=CARTESIAN_POINT('Ctrl Pts',(-2.65101366112809,0.212875307143708,
-1.38777878078145E-16));
#39693=CARTESIAN_POINT('Ctrl Pts',(-2.65226659852151,0.256588270610049,
-1.20615204739669E-16));
#39694=CARTESIAN_POINT('Ctrl Pts',(-2.65236023741492,0.300287183221066,
-4.34987190636111E-16));
#39695=CARTESIAN_POINT('Ctrl Pts',(-2.6512772014093,0.343931535522003,-4.16333634234434E-16));
#39696=CARTESIAN_POINT('Ctrl Pts',(-2.64907421925761,0.432707650667494,
-4.32903459206313E-16));
#39697=CARTESIAN_POINT('Ctrl Pts',(-2.64200629387468,0.521257644934972,
-8.62622134822235E-17));
#39698=CARTESIAN_POINT('Ctrl Pts',(-2.63031624428264,0.609320814221094,
-8.32667268468867E-17));
#39699=CARTESIAN_POINT('Ctrl Pts',(-2.61839797794639,0.699103179787949,
-8.02127613999854E-17));
#39700=CARTESIAN_POINT('Ctrl Pts',(-2.60167524897612,0.788380265268053,
1.49019320792917E-16));
#39701=CARTESIAN_POINT('Ctrl Pts',(-2.58035146554209,0.876878238745711,
2.4980018054066E-16));
#39702=CARTESIAN_POINT('Ctrl Pts',(-2.57698234718955,0.890860754912604,
2.65723370025807E-16));
#39703=CARTESIAN_POINT('Ctrl Pts',(-2.57349826551832,0.904823813068977,
1.71128026421916E-16));
#39704=CARTESIAN_POINT('Ctrl Pts',(-2.56989990586492,0.918766319054272,
1.94289029309402E-16));
#39705=CARTESIAN_POINT('Ctrl Pts',(-2.56629916621592,0.932718046770052,
2.17465351145046E-16));
#39706=CARTESIAN_POINT('Ctrl Pts',(-2.56258611805641,0.946640891227604,
-7.03868084514403E-16));
#39707=CARTESIAN_POINT('Ctrl Pts',(-2.55876298044222,0.960529869852388,
-6.93889390390723E-16));
#39708=CARTESIAN_POINT('Ctrl Pts',(-2.53419843880054,1.04976976342104,-6.29773977327716E-16));
#39709=CARTESIAN_POINT('Ctrl Pts',(-2.50508011125346,1.13766264916498,6.87890529294335E-17));
#39710=CARTESIAN_POINT('Ctrl Pts',(-2.47169823504828,1.22392740477737,8.32667268468867E-17));
#39711=CARTESIAN_POINT('Ctrl Pts',(-2.43767482619284,1.31184999582573,9.80226325947151E-17));
#39712=CARTESIAN_POINT('Ctrl Pts',(-2.39922225163329,1.39808205966622,-2.50151931196036E-16));
#39713=CARTESIAN_POINT('Ctrl Pts',(-2.35659236008881,1.48232869936419,-2.77555756156289E-16));
#39714=CARTESIAN_POINT('Ctrl Pts',(-2.31360056696885,1.56729054124849,-3.05192222745878E-16));
#39715=CARTESIAN_POINT('Ctrl Pts',(-2.26635993703635,1.65023397727082,5.65740922539343E-17));
#39716=CARTESIAN_POINT('Ctrl Pts',(-2.21507658716517,1.73084671943837,5.55111512312578E-17));
#39717=CARTESIAN_POINT('Ctrl Pts',(-2.18435464293681,1.77913880985734,5.48743828668913E-17));
#39718=CARTESIAN_POINT('Ctrl Pts',(-2.15218088295609,1.82659422289983,-3.64380860772878E-16));
#39719=CARTESIAN_POINT('Ctrl Pts',(-2.11859145320912,1.87314213253736,-3.88578058618805E-16));
#39720=CARTESIAN_POINT('Ctrl Pts',(-2.10923966749503,1.88610174750099,-3.95314910385597E-16));
#39721=CARTESIAN_POINT('Ctrl Pts',(-2.09977706809611,1.89899226435558,-9.16981750261902E-17));
#39722=CARTESIAN_POINT('Ctrl Pts',(-2.0902160744712,1.91179680016256,-1.11022302462516E-16));
#39723=CARTESIAN_POINT('Ctrl Pts',(-2.03140899114824,1.99055403331781,-2.29879778669894E-16));
#39724=CARTESIAN_POINT('Ctrl Pts',(-1.96879105165951,2.06618994280669,4.68887291460301E-17));
#39725=CARTESIAN_POINT('Ctrl Pts',(-1.90263522085423,2.13839704217079,0.));
#39726=CARTESIAN_POINT('Ctrl Pts',(-1.83630675569242,2.21079256674222,-4.70110857922477E-17));
#39727=CARTESIAN_POINT('Ctrl Pts',(-1.76642150904269,2.27974226115238,-1.93865480317173E-16));
#39728=CARTESIAN_POINT('Ctrl Pts',(-1.6932045763485,2.34492041918897,-1.66533453693773E-16));
#39729=CARTESIAN_POINT('Ctrl Pts',(-1.62138195170811,2.40885735573024,-1.39721925040515E-16));
#39730=CARTESIAN_POINT('Ctrl Pts',(-1.54635279514513,2.46916580377976,-2.38947154895597E-16));
#39731=CARTESIAN_POINT('Ctrl Pts',(-1.46828869930752,2.52551090354043,-2.77555756156289E-16));
#39732=CARTESIAN_POINT('Ctrl Pts',(-1.41016377964657,2.56746430557163,-3.06302926317174E-16));
#39733=CARTESIAN_POINT('Ctrl Pts',(-1.35035542782446,2.60721994910279,8.78385754915914E-18));
#39734=CARTESIAN_POINT('Ctrl Pts',(-1.28892185405322,2.64462557919718,0.));
#39735=CARTESIAN_POINT('Origin',(0.,0.,0.));
#39736=CARTESIAN_POINT('Origin',(-1.44337567297407,-2.5,-6.));
#39737=CARTESIAN_POINT('',(-1.44337567297407,-2.5,-6.));
#39738=CARTESIAN_POINT('',(1.44337567297406,-2.5,-6.));
#39739=CARTESIAN_POINT('',(-0.721687836487033,-2.5,-6.));
#39740=CARTESIAN_POINT('',(-1.44337567297407,-2.5,-3.));
#39741=CARTESIAN_POINT('',(-1.44337567297407,-2.5,-6.));
#39742=CARTESIAN_POINT('',(1.44337567297406,-2.5,-3.));
#39743=CARTESIAN_POINT('',(-1.44337567297407,-2.5,-3.));
#39744=CARTESIAN_POINT('',(1.44337567297406,-2.5,-6.));
#39745=CARTESIAN_POINT('Origin',(-2.88675134594813,3.53525079574969E-16,
-6.));
#39746=CARTESIAN_POINT('',(-2.88675134594813,3.53525079574969E-16,-6.));
#39747=CARTESIAN_POINT('',(-2.52590742770461,-0.625,-6.));
#39748=CARTESIAN_POINT('',(-2.88675134594813,5.55111512312578E-16,-3.));
#39749=CARTESIAN_POINT('',(-2.88675134594813,3.53525079574969E-16,-6.));
#39750=CARTESIAN_POINT('',(-2.88675134594813,3.53525079574969E-16,-3.));
#39751=CARTESIAN_POINT('Origin',(-1.44337567297406,2.5,-6.));
#39752=CARTESIAN_POINT('',(-1.44337567297406,2.5,-6.));
#39753=CARTESIAN_POINT('',(-1.80421959121758,1.875,-6.));
#39754=CARTESIAN_POINT('',(-1.44337567297406,2.5,-3.));
#39755=CARTESIAN_POINT('',(-1.44337567297406,2.5,-6.));
#39756=CARTESIAN_POINT('',(-1.44337567297406,2.5,-3.));
#39757=CARTESIAN_POINT('Origin',(1.44337567297406,2.5,-6.));
#39758=CARTESIAN_POINT('',(1.44337567297406,2.5,-6.));
#39759=CARTESIAN_POINT('',(0.721687836487033,2.5,-6.));
#39760=CARTESIAN_POINT('',(1.44337567297406,2.5,-3.));
#39761=CARTESIAN_POINT('',(1.44337567297406,2.5,-6.));
#39762=CARTESIAN_POINT('',(1.44337567297406,2.5,-3.));
#39763=CARTESIAN_POINT('Origin',(2.88675134594813,0.,-6.));
#39764=CARTESIAN_POINT('',(2.88675134594813,0.,-6.));
#39765=CARTESIAN_POINT('',(2.52590742770461,0.625,-6.));
#39766=CARTESIAN_POINT('',(2.88675134594813,0.,-3.));
#39767=CARTESIAN_POINT('',(2.88675134594813,0.,-6.));
#39768=CARTESIAN_POINT('',(2.88675134594813,0.,-3.));
#39769=CARTESIAN_POINT('Origin',(1.44337567297406,-2.5,-6.));
#39770=CARTESIAN_POINT('',(1.80421959121758,-1.875,-6.));
#39771=CARTESIAN_POINT('',(1.44337567297406,-2.5,-3.));
#39772=CARTESIAN_POINT('Origin',(0.,0.,-3.));
#39773=CARTESIAN_POINT('Origin',(0.,0.,0.));
#39774=CARTESIAN_POINT('',(-5.,-6.12323399573677E-16,0.));
#39775=CARTESIAN_POINT('Origin',(0.,0.,0.));
#39776=CARTESIAN_POINT('Origin',(0.,0.,-6.));
#39777=CARTESIAN_POINT('',(-5.,-6.12323399573677E-16,-6.));
#39778=CARTESIAN_POINT('',(-5.,-6.12323399573677E-16,-6.));
#39779=CARTESIAN_POINT('Origin',(0.,0.,-6.));
#39780=CARTESIAN_POINT('Origin',(0.,0.,-6.));
#39781=CARTESIAN_POINT('Origin',(0.,0.,12.));
#42605=UNCERTAINTY_MEASURE_WITH_UNIT(LENGTH_MEASURE(0.01),#42621,
'DISTANCE_ACCURACY_VALUE',
'Maximum model space distance between geometric entities at asserted c
onnectivities');
#42608=UNCERTAINTY_MEASURE_WITH_UNIT(LENGTH_MEASURE(0.01),#42621,
'DISTANCE_ACCURACY_VALUE',
'Maximum model space distance between geometric entities at asserted c
onnectivities');
#42617=(
GEOMETRIC_REPRESENTATION_CONTEXT(3)
GLOBAL_UNCERTAINTY_ASSIGNED_CONTEXT((#42605))
GLOBAL_UNIT_ASSIGNED_CONTEXT((#42621,#42623,#42624))
REPRESENTATION_CONTEXT('','3D')
);
#42620=(
GEOMETRIC_REPRESENTATION_CONTEXT(3)
GLOBAL_UNCERTAINTY_ASSIGNED_CONTEXT((#42608))
GLOBAL_UNIT_ASSIGNED_CONTEXT((#42621,#42623,#42624))
REPRESENTATION_CONTEXT('','3D')
);
#42621=(
LENGTH_UNIT()
NAMED_UNIT(*)
SI_UNIT(.MILLI.,.METRE.)
);
#42623=(
NAMED_UNIT(*)
PLANE_ANGLE_UNIT()
SI_UNIT($,.RADIAN.)
);
#42624=(
NAMED_UNIT(*)
SI_UNIT($,.STERADIAN.)
SOLID_ANGLE_UNIT()
);
#42633=SHAPE_DEFINITION_REPRESENTATION(#42644,#42730);
#42644=PRODUCT_DEFINITION_SHAPE('',$,#42742);
#42730=SHAPE_REPRESENTATION('',(#11115),#42617);
#42733=PRODUCT_DEFINITION_CONTEXT('part definition',#42768,'design');
#42742=PRODUCT_DEFINITION('Socket head cap screw M6x12',
'Socket head cap screw M6x12',#42753,#42733);
#42753=PRODUCT_DEFINITION_FORMATION('',$,#42778);
#42768=APPLICATION_CONTEXT(
'Core Data for Automotive Mechanical Design Process');
#42769=PRODUCT_CONTEXT('part definition',#42768,'mechanical');
#42778=PRODUCT('Socket head cap screw M6x12',
'Socket head cap screw M6x12',$,(#42769));
#42784=PRESENTATION_STYLE_ASSIGNMENT((#42792));
#42792=SURFACE_STYLE_USAGE(.BOTH.,#42800);
#42800=SURFACE_SIDE_STYLE('',(#42808));
#42808=SURFACE_STYLE_FILL_AREA(#42816);
#42816=FILL_AREA_STYLE('Dark gray',(#42824));
#42824=FILL_AREA_STYLE_COLOUR('Dark gray',#42832);
#42832=COLOUR_RGB('Dark gray',0.250980392156863,0.282352941176471,0.32156862745098);
ENDSEC;
END-ISO-10303-21;
